ISO-10303-21;
HEADER;
/* Generated by software containing ST-Developer
 * from STEP Tools, Inc. (www.steptools.com) 
 */

FILE_DESCRIPTION(
/* description */ (''),
/* implementation_level */ '2;1');

FILE_NAME(
/* name */ 'Nut_right.step',
/* time_stamp */ '2026-10-04T22:13:49-07:00',
/* author */ (''),
/* organization */ (''),
/* preprocessor_version */ 'ST-DEVELOPER v20.2',
/* originating_system */ 'Autodesk Translation Framework v15.15.0.0',
/* authorisation */ '');

FILE_SCHEMA (('AUTOMOTIVE_DESIGN { 1 0 10303 214 3 1 1 }'));
ENDSEC;

DATA;
#10=MECHANICAL_DESIGN_GEOMETRIC_PRESENTATION_REPRESENTATION('',(#368),#40734);
#47=B_SPLINE_SURFACE_WITH_KNOTS('',3,3,((#22334,#22335,#22336,#22337,#22338,
#22339,#22340,#22341,#22342,#22343,#22344,#22345,#22346,#22347,#22348,#22349,
#22350,#22351,#22352,#22353,#22354,#22355,#22356,#22357),(#22358,#22359,
#22360,#22361,#22362,#22363,#22364,#22365,#22366,#22367,#22368,#22369,#22370,
#22371,#22372,#22373,#22374,#22375,#22376,#22377,#22378,#22379,#22380,#22381),
(#22382,#22383,#22384,#22385,#22386,#22387,#22388,#22389,#22390,#22391,
#22392,#22393,#22394,#22395,#22396,#22397,#22398,#22399,#22400,#22401,#22402,
#22403,#22404,#22405),(#22406,#22407,#22408,#22409,#22410,#22411,#22412,
#22413,#22414,#22415,#22416,#22417,#22418,#22419,#22420,#22421,#22422,#22423,
#22424,#22425,#22426,#22427,#22428,#22429)),.UNSPECIFIED.,.F.,.F.,.F.,(4,
4),(4,1,1,1,1,1,1,1,1,1,1,1,1,1,1,1,1,1,1,1,1,4),(-0.000270002866089487,
0.0323833849707337),(11.8550912607133,12.8491769023077,13.8429925410361,
14.8368081797645,15.8306238184928,16.8244394572212,17.8182550959496,18.8120707346779,
19.8058863734063,20.7997020121347,21.793517650863,22.7873332895914,23.7811489283198,
24.7749645670481,25.7687802057765,26.7625958445049,27.7564114832332,28.7502271219616,
29.74404276069,30.7378583994183,31.7316740381467,32.725489676875),
 .UNSPECIFIED.);
#48=B_SPLINE_SURFACE_WITH_KNOTS('',3,3,((#22596,#22597,#22598,#22599,#22600,
#22601,#22602,#22603,#22604,#22605,#22606,#22607,#22608,#22609,#22610,#22611,
#22612,#22613,#22614,#22615,#22616,#22617,#22618,#22619),(#22620,#22621,
#22622,#22623,#22624,#22625,#22626,#22627,#22628,#22629,#22630,#22631,#22632,
#22633,#22634,#22635,#22636,#22637,#22638,#22639,#22640,#22641,#22642,#22643),
(#22644,#22645,#22646,#22647,#22648,#22649,#22650,#22651,#22652,#22653,
#22654,#22655,#22656,#22657,#22658,#22659,#22660,#22661,#22662,#22663,#22664,
#22665,#22666,#22667),(#22668,#22669,#22670,#22671,#22672,#22673,#22674,
#22675,#22676,#22677,#22678,#22679,#22680,#22681,#22682,#22683,#22684,#22685,
#22686,#22687,#22688,#22689,#22690,#22691)),.UNSPECIFIED.,.F.,.F.,.F.,(4,
4),(4,1,1,1,1,1,1,1,1,1,1,1,1,1,1,1,1,1,1,1,1,4),(-0.000235328167620964,
0.0323617480244609),(14.3982993132237,15.3922157657002,16.3860314044286,
17.379847043157,18.3736626818853,19.3674783206137,20.3612939593421,21.3551095980704,
22.3489252367988,23.3427408755272,24.3365565142555,25.3303721529839,26.3241877917123,
27.3180034304406,28.311819069169,29.3056347078974,30.2994503466257,31.2932659853541,
32.2870816240825,33.2808972628108,34.2747129015392,35.2685285402676),
 .UNSPECIFIED.);
#199=B_SPLINE_CURVE_WITH_KNOTS('',3,(#20491,#20492,#20493,#20494,#20495,
#20496),.UNSPECIFIED.,.F.,.F.,(4,1,1,4),(30.4992259586856,30.7378583994183,
31.7316740381467,32.725489676875),.UNSPECIFIED.);
#200=B_SPLINE_CURVE_WITH_KNOTS('',3,(#20499,#20500,#20501,#20502,#20503,
#20504,#20505,#20506,#20507,#20508,#20509,#20510,#20511,#20512,#20513,#20514,
#20515,#20516,#20517,#20518,#20519,#20520,#20521,#20522,#20523,#20524,#20525,
#20526,#20527,#20528,#20529,#20530,#20531,#20532,#20533,#20534,#20535,#20536,
#20537,#20538,#20539,#20540,#20541,#20542,#20543,#20544,#20545,#20546,#20547,
#20548,#20549,#20550,#20551,#20552,#20553,#20554,#20555,#20556,#20557,#20558,
#20559,#20560,#20561,#20562,#20563,#20564,#20565,#20566,#20567,#20568,#20569,
#20570,#20571,#20572,#20573,#20574),.UNSPECIFIED.,.F.,.F.,(4,3,3,3,3,3,
3,3,3,3,3,3,3,3,3,3,3,3,3,3,3,3,3,3,3,4),(30.5007265447835,30.6123224488076,
30.7238426226409,30.83533023183,30.949814170211,31.0614387973166,31.1773523913354,
31.2932659853541,31.4054181808839,31.5173715972371,31.6292139644157,31.7409880765415,
31.8527366302182,31.964582347948,32.0764735793981,32.1885741551002,32.2870816240825,
32.3984002763317,32.5095261241697,32.6205455724167,32.7315027540499,32.8424417080743,
32.953484666185,33.0645821004634,33.1758840410784,33.2477856371927),
 .UNSPECIFIED.);
#201=B_SPLINE_CURVE_WITH_KNOTS('',3,(#20580,#20581,#20582,#20583,#20584,
#20585,#20586,#20587,#20588,#20589,#20590,#20591,#20592,#20593,#20594,#20595,
#20596,#20597,#20598,#20599,#20600,#20601,#20602,#20603,#20604,#20605,#20606,
#20607,#20608,#20609,#20610,#20611,#20612,#20613,#20614,#20615,#20616,#20617,
#20618,#20619,#20620,#20621,#20622,#20623,#20624,#20625,#20626,#20627,#20628,
#20629,#20630,#20631,#20632,#20633,#20634,#20635,#20636,#20637,#20638,#20639,
#20640,#20641,#20642,#20643,#20644,#20645,#20646,#20647,#20648,#20649,#20650,
#20651,#20652,#20653,#20654,#20655,#20656,#20657,#20658,#20659,#20660,#20661,
#20662,#20663,#20664,#20665,#20666,#20667,#20668,#20669,#20670,#20671,#20672,
#20673,#20674,#20675,#20676,#20677,#20678,#20679,#20680,#20681,#20682,#20683,
#20684,#20685,#20686,#20687,#20688,#20689,#20690,#20691),.UNSPECIFIED.,
 .F.,.F.,(4,3,3,3,3,3,3,3,3,3,3,3,3,3,3,3,3,3,3,3,3,3,3,3,3,3,3,3,3,3,3,
3,3,3,3,3,3,4),(24.2171454613693,24.328721144631,24.4403944911041,24.5521112223609,
24.6640460242382,24.7749645670481,24.8869276730768,24.9986930187964,25.1103480734547,
25.2219359515843,25.3334996710813,25.445164216606,25.5568760037622,25.6688023337555,
25.7687802057765,25.8807705272124,25.9925629669429,26.1042450229036,26.2158597642098,
26.3274501632448,26.4391408893548,26.5508786252935,26.6628301813545,26.7625958445049,
26.8745738108416,26.9863543659224,27.0980248308916,27.2096282913631,27.3212077365666,
27.4328881016498,27.5446157852499,27.6565579314224,27.7564114832332,27.8730056569828,
27.989278435079,28.1053581204607,28.2212227044162,28.2743338823081),
 .UNSPECIFIED.);
#202=B_SPLINE_CURVE_WITH_KNOTS('',3,(#20692,#20693,#20694,#20695,#20696,
#20697),.UNSPECIFIED.,.F.,.F.,(4,1,1,4),(28.2743353560929,28.7502271219616,
29.74404276069,30.4992259586856),.UNSPECIFIED.);
#203=B_SPLINE_CURVE_WITH_KNOTS('',3,(#20699,#20700,#20701,#20702,#20703,
#20704,#20705,#20706,#20707,#20708,#20709,#20710,#20711,#20712,#20713,#20714,
#20715,#20716,#20717,#20718,#20719,#20720,#20721,#20722,#20723,#20724,#20725,
#20726,#20727,#20728,#20729,#20730,#20731,#20732,#20733,#20734,#20735,#20736,
#20737,#20738,#20739,#20740,#20741,#20742,#20743,#20744,#20745,#20746,#20747,
#20748,#20749,#20750,#20751,#20752,#20753,#20754,#20755,#20756,#20757,#20758,
#20759,#20760,#20761,#20762),.UNSPECIFIED.,.F.,.F.,(4,3,3,3,3,3,3,3,3,3,
3,3,3,3,3,3,3,3,3,3,3,4),(28.2743338823081,28.311819069169,28.4238093895684,
28.5356018282781,28.6472838832279,28.7588986235352,28.8704890215845,28.9821797467369,
29.0939174817321,29.2058690368848,29.3056347078974,29.417612671015,29.5293932228493,
29.6410636845579,29.7526671417604,29.8642465836919,29.9759269455253,30.0876546258826,
30.1995967688657,30.2994503466257,30.4113016433696,30.5007265447835),
 .UNSPECIFIED.);
#204=B_SPLINE_CURVE_WITH_KNOTS('',3,(#20763,#20764,#20765,#20766,#20767,
#20768,#20769,#20770,#20771,#20772,#20773,#20774,#20775,#20776,#20777,#20778,
#20779,#20780,#20781,#20782,#20783,#20784,#20785,#20786,#20787,#20788,#20789,
#20790,#20791,#20792,#20793,#20794,#20795,#20796,#20797,#20798,#20799,#20800,
#20801,#20802,#20803,#20804,#20805,#20806,#20807,#20808,#20809,#20810,#20811,
#20812,#20813,#20814,#20815,#20816,#20817,#20818,#20819,#20820,#20821,#20822,
#20823,#20824,#20825,#20826,#20827,#20828,#20829,#20830,#20831,#20832,#20833,
#20834,#20835,#20836,#20837,#20838,#20839,#20840,#20841,#20842,#20843,#20844,
#20845,#20846,#20847,#20848,#20849,#20850,#20851,#20852,#20853,#20854,#20855,
#20856,#20857,#20858,#20859,#20860,#20861,#20862,#20863,#20864,#20865,#20866,
#20867,#20868,#20869,#20870,#20871,#20872,#20873,#20874,#20875,#20876,#20877),
 .UNSPECIFIED.,.F.,.F.,(4,3,3,3,3,3,3,3,3,3,3,3,3,3,3,3,3,3,3,3,3,3,3,3,
3,3,3,3,3,3,3,3,3,3,3,3,3,3,4),(24.2164750170476,24.3284524197536,24.3365565142555,
24.4485275333045,24.5603007790059,24.6719637201736,24.7835594578674,24.8951309964992,
25.0068032353764,25.1185226592433,25.2304564321671,25.3303721529839,25.4423470704048,
25.5541242241199,25.6657910764357,25.7773907217266,25.8889661577255,26.000642246938,
26.1123655015154,26.2243030228786,26.3241877917123,26.4361623320395,26.5479391606963,
26.659605719745,26.7712051037159,26.8827803105362,26.9944562220728,27.1061793269458,
27.2181167469796,27.3180034304406,27.4292987988986,27.5403976766296,27.6513879633006,
27.7623138516846,27.8732194375054,27.9842247077935,28.0952828235162,28.2065395519308,
28.2743338817731),.UNSPECIFIED.);
#205=B_SPLINE_CURVE_WITH_KNOTS('',3,(#20883,#20884,#20885,#20886,#20887,
#20888,#20889,#20890,#20891,#20892,#20893,#20894,#20895,#20896,#20897,#20898,
#20899,#20900,#20901,#20902,#20903,#20904,#20905,#20906,#20907,#20908,#20909,
#20910,#20911,#20912,#20913,#20914,#20915,#20916,#20917,#20918,#20919,#20920,
#20921,#20922,#20923,#20924,#20925,#20926,#20927,#20928,#20929,#20930,#20931,
#20932,#20933,#20934,#20935,#20936,#20937,#20938,#20939,#20940,#20941,#20942,
#20943),.UNSPECIFIED.,.F.,.F.,(4,3,3,3,3,3,3,3,3,3,3,3,3,3,3,3,3,3,3,3,
4),(15.707963267949,15.8187595067976,15.9295233360101,16.0436503531147,
16.1545574801957,16.2702944423121,16.3860314044286,16.4979936760791,16.6097538040557,
16.7214009788804,16.8329783413831,16.9445289325292,17.0561763685529,17.1678688344864,
17.2797723742714,17.379847043157,17.4919754947928,17.6039188766938,17.7157519036505,
17.8275438837686,17.9335641972525),.UNSPECIFIED.);
#206=B_SPLINE_CURVE_WITH_KNOTS('',3,(#20945,#20946,#20947,#20948,#20949,
#20950,#20951,#20952,#20953,#20954,#20955,#20956,#20957,#20958,#20959,#20960,
#20961,#20962,#20963,#20964,#20965,#20966,#20967,#20968,#20969,#20970,#20971,
#20972,#20973,#20974,#20975,#20976,#20977,#20978,#20979,#20980,#20981),
 .UNSPECIFIED.,.F.,.F.,(4,3,3,3,3,3,3,3,3,3,3,3,4),(14.3984001269719,14.5126517902779,
14.6268360531343,14.7409856972805,14.8551365966922,14.9693246155366,15.0836816294035,
15.1981262282676,15.3128130782455,15.3922157657002,15.5228352705414,15.6520281526537,
15.7079632674506),.UNSPECIFIED.);
#207=B_SPLINE_CURVE_WITH_KNOTS('',3,(#20985,#20986,#20987,#20988,#20989,
#20990,#20991,#20992,#20993,#20994,#20995,#20996,#20997,#20998,#20999,#21000,
#21001,#21002,#21003,#21004,#21005,#21006,#21007,#21008,#21009,#21010,#21011,
#21012,#21013,#21014,#21015,#21016,#21017,#21018,#21019,#21020,#21021,#21022,
#21023,#21024,#21025,#21026,#21027,#21028,#21029,#21030,#21031,#21032,#21033,
#21034,#21035,#21036),.UNSPECIFIED.,.F.,.F.,(4,3,3,3,3,3,3,3,3,3,3,3,3,
3,3,3,3,4),(13.8759341327667,13.9872665954873,14.0984010834278,14.2094259872279,
14.3203854485755,14.4313235110963,14.5423608000363,14.6534498395139,14.7647392915059,
14.8368081797645,14.9473443597248,15.0577306248179,15.1680122762973,15.2782344500762,
15.3885087645923,15.4988033613755,15.6092745562469,15.7079632675072),
 .UNSPECIFIED.);
#208=B_SPLINE_CURVE_WITH_KNOTS('',3,(#21037,#21038,#21039,#21040,#21041,
#21042,#21043,#21044,#21045,#21046,#21047,#21048,#21049,#21050,#21051,#21052,
#21053,#21054,#21055,#21056,#21057,#21058,#21059,#21060,#21061,#21062,#21063,
#21064,#21065,#21066,#21067,#21068,#21069,#21070,#21071,#21072,#21073,#21074,
#21075,#21076,#21077,#21078,#21079,#21080,#21081,#21082,#21083,#21084,#21085,
#21086,#21087,#21088,#21089,#21090,#21091,#21092,#21093,#21094,#21095,#21096,
#21097),.UNSPECIFIED.,.F.,.F.,(4,3,3,3,3,3,3,3,3,3,3,3,3,3,3,3,3,3,3,3,
4),(15.707963267949,15.8306238184928,15.9425134931221,16.0542037235325,
16.1657826907118,16.2772936442665,16.3887797359164,16.5003661757896,16.6119994681162,
16.7238476652717,16.8244394572212,16.9364188879014,17.0482003665379,17.1598714256532,
17.2714751517678,17.3830545346207,17.4947343260332,17.6064611544644,17.7184019844554,
17.8182550959496,17.9342486843494),.UNSPECIFIED.);
#209=B_SPLINE_CURVE_WITH_KNOTS('',3,(#21103,#21104,#21105,#21106,#21107,
#21108,#21109,#21110,#21111,#21112,#21113,#21114,#21115,#21116,#21117,#21118,
#21119,#21120,#21121,#21122,#21123,#21124,#21125,#21126,#21127,#21128,#21129,
#21130,#21131,#21132,#21133,#21134,#21135,#21136,#21137,#21138,#21139,#21140,
#21141,#21142,#21143,#21144,#21145,#21146,#21147,#21148,#21149,#21150,#21151,
#21152,#21153,#21154),.UNSPECIFIED.,.F.,.F.,(4,3,3,3,3,3,3,3,3,3,3,3,3,
3,3,3,3,4),(18.2325677587798,18.3498303574559,18.4670738156485,18.5844332834504,
18.7018559905836,18.8195012614516,18.8824971358389,18.9993814731626,19.1160527382571,
19.2326074989738,19.3490972166108,19.4655732408159,19.5821766235442,19.6988502996544,
19.8157586904299,19.8763127745673,20.0296181157692,20.1591059545013),
 .UNSPECIFIED.);
#210=B_SPLINE_CURVE_WITH_KNOTS('',3,(#21156,#21157,#21158,#21159,#21160,
#21161,#21162,#21163,#21164,#21165,#21166,#21167,#21168,#21169),
 .UNSPECIFIED.,.F.,.F.,(4,2,2,2,2,2,4),(-0.0903144895684469,-0.0692444659278893,
-0.0576954263704227,-0.0451675812950829,-0.0304576276691574,-0.00758134388617478,
0.),.UNSPECIFIED.);
#211=B_SPLINE_CURVE_WITH_KNOTS('',3,(#21172,#21173,#21174,#21175,#21176,
#21177,#21178,#21179,#21180,#21181,#21182,#21183,#21184,#21185,#21186,#21187,
#21188,#21189,#21190,#21191,#21192,#21193,#21194,#21195,#21196,#21197,#21198,
#21199,#21200,#21201,#21202,#21203,#21204,#21205,#21206,#21207,#21208,#21209,
#21210,#21211,#21212,#21213,#21214,#21215,#21216,#21217,#21218,#21219,#21220,
#21221,#21222,#21223,#21224,#21225,#21226,#21227,#21228,#21229,#21230,#21231,
#21232,#21233,#21234,#21235,#21236,#21237,#21238,#21239,#21240,#21241,#21242,
#21243,#21244,#21245,#21246,#21247,#21248,#21249,#21250,#21251),
 .UNSPECIFIED.,.F.,.F.,(4,2,2,2,2,2,2,2,2,2,2,2,2,2,2,2,2,2,2,2,2,2,2,2,
2,2,2,2,2,2,2,2,2,2,2,2,2,2,2,4),(-2.38727423776056,-2.38406272448339,-2.3557931220579,
-2.33755291028634,-2.32704088174431,-2.31484332484773,-2.28541728558956,
-2.27583295603182,-2.26827320890842,-2.26174684622007,-2.23039420085245,
-2.21738636427069,-2.20583957855992,-2.19513154387513,-2.17099129080296,
-2.15495721776536,-2.14472291534183,-2.13868394797197,-2.12944141110975,
-2.10363838951637,-2.09095738686218,-2.07961062057348,-2.06898426027192,
-2.04490653827237,-2.02884653579313,-2.01862053881223,-2.0126050191353,
-2.0034594802115,-1.97766500598942,-1.96487183705672,-1.95344529599827,
-1.94275622036405,-1.92404139176448,-1.9045009960413,-1.89321241694263,
-1.88718106050413,-1.87861020022266,-1.85185187742313,-1.83903298230054,
-1.83671080313269),.UNSPECIFIED.);
#212=B_SPLINE_CURVE_WITH_KNOTS('',3,(#21257,#21258,#21259,#21260,#21261,
#21262,#21263,#21264,#21265,#21266,#21267,#21268,#21269,#21270,#21271,#21272,
#21273,#21274,#21275,#21276,#21277,#21278,#21279,#21280,#21281,#21282,#21283,
#21284,#21285,#21286,#21287,#21288,#21289,#21290,#21291,#21292,#21293,#21294,
#21295,#21296,#21297,#21298,#21299,#21300,#21301,#21302,#21303,#21304,#21305,
#21306,#21307,#21308,#21309,#21310,#21311),.UNSPECIFIED.,.F.,.F.,(4,3,3,
3,3,3,3,3,3,3,3,3,3,3,3,3,3,3,4),(11.9490926668048,12.0704064963878,12.1878478712382,
12.3051825606139,12.4224605559092,12.5397317517184,12.6571250989989,12.7745928009127,
12.8922685579825,12.9196033034688,13.039144609872,13.1559019011595,13.2725441076707,
13.3891225237288,13.5108253314701,13.6275077647654,13.7442638674747,13.8612193036346,
13.8759337546943),.UNSPECIFIED.);
#213=B_SPLINE_CURVE_WITH_KNOTS('',3,(#21312,#21313,#21314,#21315,#21316,
#21317,#21318,#21319,#21320,#21321,#21322,#21323,#21324,#21325,#21326,#21327,
#21328,#21329,#21330,#21331,#21332,#21333,#21334,#21335,#21336,#21337,#21338,
#21339,#21340,#21341,#21342,#21343,#21344,#21345,#21346,#21347,#21348,#21349,
#21350,#21351,#21352,#21353,#21354,#21355,#21356,#21357,#21358,#21359,#21360,
#21361,#21362,#21363,#21364,#21365,#21366,#21367,#21368,#21369,#21370,#21371,
#21372,#21373,#21374,#21375,#21376,#21377,#21378,#21379,#21380,#21381,#21382,
#21383,#21384,#21385,#21386,#21387,#21388,#21389,#21390,#21391,#21392,#21393,
#21394,#21395,#21396,#21397,#21398,#21399,#21400,#21401,#21402,#21403,#21404,
#21405,#21406,#21407,#21408,#21409,#21410,#21411,#21412,#21413,#21414,#21415,
#21416,#21417,#21418,#21419,#21420,#21421,#21422,#21423,#21424,#21425,#21426,
#21427,#21428,#21429,#21430,#21431,#21432),.UNSPECIFIED.,.F.,.F.,(4,3,3,
3,3,3,3,3,3,3,3,3,3,3,3,3,3,3,3,3,3,3,3,3,3,3,3,3,3,3,3,3,3,3,3,3,3,3,3,
3,4),(13.8759337553363,13.9134189421971,14.0311232235957,14.1486125013357,
14.2659834897556,14.3832861820323,14.5005704595919,14.6179686096979,14.7354306420707,
14.853108166008,14.9072345809255,15.0249258745496,15.1424026742923,15.2597615104701,
15.3770523954505,15.4943252302791,15.6117125694428,15.7291641366733,15.8468318409145,
15.9010502196539,16.0186444543146,16.1360236186112,16.2532845471506,16.3704774396887,
16.4876523842386,16.6049427606468,16.7222977569782,16.8398706110872,16.8948658583822,
17.0127402740903,17.1303987141068,17.2479381064766,17.3654081250404,17.4828583308553,
17.6004190050346,17.7180418335406,17.8358756688541,17.8886814971106,18.0063081000976,
18.1237490007858,18.2325677587798),.UNSPECIFIED.);
#214=B_SPLINE_CURVE_WITH_KNOTS('',3,(#21433,#21434,#21435,#21436,#21437,
#21438,#21439,#21440,#21441,#21442,#21443,#21444,#21445,#21446,#21447,#21448,
#21449,#21450,#21451,#21452,#21453,#21454,#21455,#21456,#21457,#21458,#21459,
#21460,#21461,#21462,#21463,#21464,#21465,#21466,#21467,#21468,#21469,#21470,
#21471,#21472,#21473,#21474,#21475,#21476,#21477,#21478,#21479,#21480,#21481,
#21482,#21483,#21484,#21485,#21486,#21487,#21488,#21489,#21490,#21491,#21492,
#21493,#21494,#21495,#21496,#21497,#21498,#21499,#21500,#21501,#21502,#21503,
#21504,#21505,#21506,#21507,#21508,#21509,#21510,#21511,#21512,#21513,#21514,
#21515,#21516,#21517,#21518,#21519,#21520,#21521,#21522,#21523,#21524,#21525,
#21526,#21527,#21528,#21529,#21530,#21531,#21532,#21533,#21534,#21535,#21536,
#21537,#21538,#21539,#21540,#21541,#21542,#21543,#21544,#21545,#21546),
 .UNSPECIFIED.,.F.,.F.,(4,2,2,2,2,2,2,2,2,2,2,2,2,2,2,2,2,2,2,2,2,2,2,2,
2,2,2,2,2,2,2,2,2,2,2,2,2,2,2,2,2,2,2,2,2,2,2,2,2,2,2,2,2,2,2,2,4),(-1.83671080313269,
-1.82759849494319,-1.81692795186113,-1.79563929798103,-1.77779257395854,
-1.76699053250404,-1.76093911515616,-1.75209456774871,-1.72642332328398,
-1.71339291330754,-1.70186211436507,-1.69125802302839,-1.67198737355153,
-1.6525162997874,-1.64426846678166,-1.63741779966473,-1.63057719938065,
-1.61111305684996,-1.58624264998279,-1.575038216497,-1.56423320731616,-1.53294347082481,
-1.51676689755966,-1.51040659458799,-1.5028295689763,-1.47285225044348,
-1.46041985100477,-1.44917306242916,-1.43840209278037,-1.42139887540163,
-1.40094682104524,-1.389416018895,-1.38332969003068,-1.37485962772093,-1.33992511892625,
-1.32670780248308,-1.31643728663368,-1.30152516541418,-1.27648087306842,
-1.26389145275289,-1.2577415241614,-1.249492316077,-1.22423903595011,-1.20491784183702,
-1.19442406440538,-1.1826084706153,-1.16897540982433,-1.14368559895163,
-1.13545766355708,-1.12939283725948,-1.11738157832569,-1.09498355884621,
-1.07799856687676,-1.06762641984851,-1.0553136942615,-1.04059910634095,
-1.04037338208336),.UNSPECIFIED.);
#215=B_SPLINE_CURVE_WITH_KNOTS('',3,(#21552,#21553,#21554,#21555,#21556,
#21557,#21558,#21559,#21560,#21561,#21562,#21563,#21564,#21565,#21566,#21567,
#21568,#21569,#21570,#21571,#21572,#21573,#21574,#21575,#21576,#21577,#21578,
#21579,#21580,#21581,#21582,#21583,#21584,#21585),.UNSPECIFIED.,.F.,.F.,
(4,2,2,2,2,2,2,2,2,2,2,2,2,2,2,2,4),(-0.244154988360166,-0.239251614829434,
-0.206955793200255,-0.193245893310612,-0.183335383234761,-0.17038967951317,
-0.135910395886769,-0.127712618705488,-0.121625554061406,-0.110199764636449,
-0.0909155361461006,-0.0686614677051733,-0.0570683697132675,-0.0439652197544473,
-0.0280399100598725,-0.0077322087934803,-3.42095323259393E-5),
 .UNSPECIFIED.);
#216=B_SPLINE_CURVE_WITH_KNOTS('',3,(#21588,#21589,#21590,#21591,#21592,
#21593,#21594,#21595,#21596,#21597,#21598,#21599,#21600,#21601,#21602,#21603,
#21604,#21605,#21606,#21607,#21608,#21609,#21610,#21611,#21612,#21613,#21614,
#21615,#21616,#21617,#21618,#21619,#21620,#21621,#21622,#21623,#21624,#21625,
#21626,#21627,#21628,#21629,#21630,#21631,#21632,#21633,#21634,#21635,#21636,
#21637,#21638,#21639,#21640,#21641,#21642,#21643,#21644,#21645,#21646,#21647,
#21648,#21649,#21650,#21651,#21652,#21653,#21654,#21655,#21656,#21657,#21658,
#21659,#21660,#21661,#21662,#21663,#21664,#21665,#21666,#21667,#21668,#21669,
#21670,#21671,#21672,#21673,#21674,#21675,#21676,#21677,#21678,#21679,#21680,
#21681,#21682,#21683,#21684,#21685,#21686,#21687),.UNSPECIFIED.,.F.,.F.,
(4,3,3,3,3,3,3,3,3,3,3,3,3,3,3,3,3,3,3,3,3,3,3,3,3,3,3,3,3,3,3,3,3,4),(2.02058687755678,
2.14069438238532,2.2574883425309,2.37416635199786,2.49077964507473,2.61344646285233,
2.73016277784316,2.84695211083585,2.96394200550359,2.9814469161851,3.09930457100341,
3.21695263862805,3.33448562654666,3.45195319760804,3.56940490710038,3.68697299397692,
3.80460662818603,3.92245632155603,3.97526255491346,4.09286106442566,4.21024287633558,
4.32750544285481,4.44469896657569,4.56187353699821,4.67916203298068,4.79651428555477,
4.91408310460292,4.96907819364183,5.08674497378225,5.2042322284644,5.32160189552125,
5.43889690344537,5.55623184519139,5.66526454987602),.UNSPECIFIED.);
#217=B_SPLINE_CURVE_WITH_KNOTS('',3,(#21690,#21691,#21692,#21693,#21694,
#21695,#21696,#21697,#21698,#21699,#21700,#21701,#21702,#21703,#21704,#21705,
#21706,#21707,#21708,#21709,#21710,#21711,#21712,#21713,#21714,#21715,#21716,
#21717,#21718,#21719,#21720,#21721,#21722,#21723,#21724,#21725,#21726,#21727,
#21728,#21729,#21730,#21731,#21732,#21733,#21734,#21735,#21736,#21737,#21738,
#21739,#21740,#21741,#21742,#21743,#21744),.UNSPECIFIED.,.F.,.F.,(4,3,3,
3,3,3,3,3,3,3,3,3,3,3,3,3,3,3,4),(5.66526454987602,5.78270914137197,5.90037195798557,
5.9628938323702,6.08059634138301,6.19808452175179,6.31545483179508,6.4327572635203,
6.55004169773963,6.66744062916035,6.78490380112927,6.90258299960002,6.95670947109856,
7.07493575073346,7.19296502881277,7.31083750640158,7.42861915180826,7.54637977656283,
7.59274844815668),.UNSPECIFIED.);
#218=B_SPLINE_CURVE_WITH_KNOTS('',3,(#21745,#21746,#21747,#21748,#21749,
#21750,#21751,#21752,#21753,#21754,#21755,#21756,#21757,#21758,#21759,#21760,
#21761,#21762,#21763,#21764,#21765,#21766,#21767,#21768,#21769,#21770,#21771,
#21772,#21773,#21774,#21775,#21776,#21777,#21778,#21779,#21780,#21781,#21782,
#21783,#21784,#21785,#21786,#21787,#21788,#21789,#21790,#21791,#21792,#21793,
#21794,#21795,#21796,#21797,#21798,#21799,#21800,#21801,#21802,#21803,#21804,
#21805,#21806,#21807,#21808,#21809,#21810,#21811,#21812,#21813,#21814,#21815,
#21816,#21817,#21818,#21819,#21820,#21821,#21822,#21823,#21824,#21825,#21826,
#21827,#21828,#21829,#21830,#21831,#21832,#21833,#21834,#21835,#21836,#21837,
#21838,#21839,#21840,#21841,#21842,#21843,#21844,#21845,#21846,#21847,#21848,
#21849,#21850,#21851,#21852,#21853,#21854,#21855,#21856,#21857,#21858,#21859,
#21860,#21861,#21862,#21863,#21864,#21865),.UNSPECIFIED.,.F.,.F.,(4,3,3,
3,3,3,3,3,3,3,3,3,3,3,3,3,3,3,3,3,3,3,3,3,3,3,3,3,3,3,3,3,3,3,3,3,3,3,3,
3,4),(7.59274844886418,7.72611340783759,7.86064797894208,7.95052510982693,
8.06821292749181,8.18568587942327,8.30304064157112,8.42032723670827,8.53759557598362,
8.65497815000861,8.77242479148122,8.89008738406618,8.94434074855529,9.06202865632316,
9.17950175858101,9.2968567083081,9.4141435278905,9.53141212813995,9.64879501639168,
9.76624200300912,9.88390498447909,9.93815638728366,10.0558403825393,10.1733094914499,
10.2906604012616,10.4079431422432,10.5252076330259,10.64258639774,10.7600292469684,
10.8776881175203,10.931972026012,11.0496601185419,11.1671333352003,11.2844883556557,
11.4017752024163,11.5190437863578,11.6364265931865,11.753873461037,11.8715362679689,
11.9257876647404,11.9490926668048),.UNSPECIFIED.);
#219=B_SPLINE_CURVE_WITH_KNOTS('',3,(#21866,#21867,#21868,#21869,#21870,
#21871,#21872,#21873,#21874,#21875,#21876,#21877,#21878,#21879,#21880,#21881,
#21882,#21883,#21884,#21885,#21886,#21887,#21888,#21889,#21890,#21891,#21892,
#21893,#21894,#21895,#21896,#21897,#21898,#21899,#21900,#21901,#21902,#21903,
#21904,#21905,#21906,#21907,#21908,#21909,#21910,#21911,#21912,#21913,#21914,
#21915,#21916,#21917,#21918,#21919,#21920,#21921,#21922,#21923,#21924,#21925,
#21926,#21927,#21928,#21929,#21930,#21931,#21932,#21933,#21934,#21935,#21936,
#21937,#21938,#21939,#21940,#21941,#21942,#21943,#21944,#21945,#21946,#21947,
#21948,#21949,#21950,#21951,#21952,#21953,#21954,#21955,#21956,#21957,#21958,
#21959,#21960,#21961,#21962,#21963,#21964,#21965,#21966,#21967,#21968,#21969,
#21970,#21971,#21972,#21973,#21974,#21975,#21976,#21977,#21978,#21979,#21980,
#21981),.UNSPECIFIED.,.F.,.F.,(4,2,2,2,2,2,2,2,2,2,2,2,2,2,2,2,2,2,2,2,
2,2,2,2,2,2,2,2,2,2,2,2,2,2,2,2,2,2,2,2,2,2,2,2,2,2,2,2,2,2,2,2,2,2,2,2,
2,4),(-1.04037338208336,-1.01416486516127,-1.00744323031407,-1.00046946854683,
-0.982039197890212,-0.955050450349102,-0.944205438114775,-0.933083306916604,
-0.920904741459413,-0.89275188124582,-0.884043275220523,-0.877984441360367,
-0.86695472795474,-0.848332082510172,-0.828046102010566,-0.817400977669383,
-0.805932927745472,-0.793039841365782,-0.767332053338507,-0.758341227968803,
-0.752290486521731,-0.741660020946498,-0.724361000924324,-0.702356242192692,
-0.691680270784957,-0.680246589919544,-0.667433930200241,-0.640695271885177,
-0.632132676579121,-0.626083321967545,-0.614911668518366,-0.595773221647233,
-0.576054912027885,-0.565466688275944,-0.554063772130212,-0.541261442307823,
-0.515538966811059,-0.506474430913304,-0.500432128228809,-0.489967423045582,
-0.473230155228666,-0.450247884308502,-0.439529294467034,-0.428019884225815,
-0.415086509727082,-0.389363599518028,-0.380374027295732,-0.374236477857763,
-0.363021236863976,-0.34370408892813,-0.32493567686722,-0.314248850844133,
-0.302594879257175,-0.289393172738,-0.263741215039427,-0.254941422894619,
-0.249100921729546,-0.244154988360166),.UNSPECIFIED.);
#220=B_SPLINE_CURVE_WITH_KNOTS('',3,(#21984,#21985,#21986,#21987,#21988,
#21989,#21990,#21991,#21992,#21993,#21994,#21995,#21996,#21997,#21998,#21999,
#22000,#22001,#22002,#22003,#22004,#22005,#22006,#22007,#22008,#22009,#22010,
#22011,#22012,#22013,#22014,#22015,#22016,#22017,#22018,#22019,#22020,#22021,
#22022,#22023,#22024,#22025,#22026,#22027,#22028,#22029,#22030,#22031,#22032,
#22033,#22034,#22035,#22036,#22037,#22038,#22039,#22040,#22041,#22042,#22043,
#22044,#22045,#22046,#22047,#22048,#22049,#22050,#22051,#22052,#22053,#22054,
#22055,#22056,#22057,#22058,#22059,#22060,#22061,#22062,#22063,#22064,#22065,
#22066,#22067,#22068,#22069,#22070,#22071,#22072,#22073,#22074,#22075,#22076,
#22077,#22078,#22079,#22080,#22081,#22082,#22083,#22084,#22085,#22086,#22087,
#22088,#22089,#22090,#22091,#22092,#22093,#22094,#22095),.UNSPECIFIED.,
 .F.,.F.,(4,3,3,3,3,3,3,3,3,3,3,3,3,3,3,3,3,3,3,3,3,3,3,3,3,3,3,3,3,3,3,
3,3,3,3,3,3,4),(17.9342486843494,18.0460353769573,18.1577136094561,18.2693264455941,
18.3809168546533,18.4926092698599,18.6043503990142,18.7163045388962,18.8120707346779,
18.9240343718639,19.0358000525972,19.1474553228003,19.2590432973348,19.3706069942819,
19.4822713317926,19.5939828088423,19.7059086614885,19.8058863734063,19.9178610297847,
20.0296379318187,20.1413045382507,20.2529039436819,20.3644791460784,20.476155012835,
20.5878780507119,20.6998153673571,20.7997020121347,20.9116767539539,21.023453796993,
21.13512057818,21.2467201917801,21.3582956354648,21.4699717937486,21.5816951511915,
21.6936328307661,21.793517650863,21.9536039852106,21.9911485751285),
 .UNSPECIFIED.);
#221=B_SPLINE_CURVE_WITH_KNOTS('',3,(#22096,#22097,#22098,#22099,#22100,
#22101,#22102,#22103,#22104,#22105,#22106,#22107,#22108,#22109,#22110,#22111,
#22112,#22113,#22114,#22115,#22116,#22117,#22118,#22119,#22120,#22121,#22122,
#22123,#22124,#22125,#22126,#22127,#22128,#22129,#22130,#22131,#22132,#22133,
#22134,#22135,#22136,#22137,#22138,#22139,#22140,#22141,#22142,#22143,#22144,
#22145,#22146,#22147,#22148,#22149,#22150,#22151,#22152,#22153,#22154,#22155,
#22156,#22157,#22158,#22159),.UNSPECIFIED.,.F.,.F.,(4,3,3,3,3,3,3,3,3,3,
3,3,3,3,3,3,3,3,3,3,3,4),(21.9911485755232,22.1013010399507,22.2113543241301,
22.321353793377,22.4313447204739,22.5414427825285,22.6516063753035,22.7619557132656,
22.7873332895914,22.8993082072233,23.011085361148,23.1227522136722,23.2343518591702,
23.3459272953745,23.457603384788,23.5693266395644,23.6812641611206,23.7811489283198,
23.8930847227604,24.0048672469585,24.1165374946164,24.2171454613693),
 .UNSPECIFIED.);
#222=B_SPLINE_CURVE_WITH_KNOTS('',3,(#22161,#22162,#22163,#22164,#22165,
#22166,#22167,#22168,#22169,#22170,#22171,#22172,#22173,#22174,#22175,#22176,
#22177,#22178,#22179,#22180,#22181,#22182,#22183,#22184,#22185,#22186,#22187,
#22188,#22189,#22190,#22191,#22192,#22193,#22194,#22195,#22196,#22197,#22198,
#22199,#22200,#22201,#22202,#22203,#22204,#22205,#22206,#22207,#22208,#22209,
#22210,#22211,#22212,#22213,#22214,#22215,#22216,#22217,#22218,#22219,#22220,
#22221),.UNSPECIFIED.,.F.,.F.,(4,3,3,3,3,3,3,3,3,3,3,3,3,3,3,3,3,3,3,3,
4),(21.9911485755562,22.1180393250501,22.2460227144172,22.3489252367988,
22.460899892698,22.5726767942465,22.6843434001895,22.795942805129,22.9075180070322,
23.0191938732966,23.1309169106812,23.2428542268404,23.3427408755272,23.4546767726727,
23.5664551376927,23.6781192288063,23.7897121490916,23.9013304775244,24.0129558539189,
24.124723624456,24.2164750170476),.UNSPECIFIED.);
#223=B_SPLINE_CURVE_WITH_KNOTS('',3,(#22222,#22223,#22224,#22225,#22226,
#22227,#22228,#22229,#22230,#22231,#22232,#22233,#22234,#22235,#22236,#22237,
#22238,#22239,#22240,#22241,#22242,#22243,#22244,#22245,#22246,#22247,#22248,
#22249,#22250,#22251,#22252,#22253,#22254,#22255,#22256,#22257,#22258,#22259,
#22260,#22261,#22262,#22263,#22264,#22265,#22266,#22267,#22268,#22269,#22270,
#22271,#22272,#22273,#22274,#22275,#22276,#22277,#22278,#22279,#22280,#22281,
#22282,#22283,#22284,#22285,#22286,#22287,#22288,#22289,#22290,#22291,#22292,
#22293,#22294,#22295,#22296,#22297,#22298,#22299,#22300,#22301,#22302,#22303,
#22304,#22305,#22306,#22307,#22308,#22309,#22310,#22311,#22312,#22313,#22314,
#22315,#22316,#22317,#22318,#22319,#22320,#22321,#22322,#22323,#22324,#22325,
#22326,#22327,#22328,#22329,#22330,#22331,#22332,#22333),.UNSPECIFIED.,
 .F.,.F.,(4,3,3,3,3,3,3,3,3,3,3,3,3,3,3,3,3,3,3,3,3,3,3,3,3,3,3,3,3,3,3,
3,3,3,3,3,3,4),(17.9335641972525,18.0454147314152,18.1573118896217,18.2694253463682,
18.3736626818853,18.4855523651012,18.5972426043066,18.708821580402,18.8203325429781,
18.9318186437399,19.0434050927939,19.155038394354,19.2668866007134,19.3674783206137,
19.4794577481211,19.5912392235406,19.7029102794142,19.8145140022681,19.9260933818471,
20.0377731699916,20.1494999951527,20.2614408219124,20.3612939593421,20.4732825933969,
20.5850739685693,20.6967553393691,20.80836977387,20.9199602438703,21.0316516298248,
21.1433903498293,21.2553434208536,21.3551095980704,21.4675965762727,21.5799041453604,
21.6920651091871,21.8041390505535,21.9161934578611,21.9911485751285),
 .UNSPECIFIED.);
#224=B_SPLINE_CURVE_WITH_KNOTS('',3,(#22431,#22432,#22433,#22434,#22435,
#22436,#22437,#22438,#22439,#22440,#22441,#22442,#22443,#22444,#22445,#22446,
#22447,#22448,#22449,#22450,#22451,#22452,#22453,#22454,#22455,#22456,#22457,
#22458,#22459,#22460,#22461,#22462,#22463,#22464,#22465,#22466,#22467,#22468,
#22469,#22470,#22471,#22472,#22473,#22474,#22475,#22476,#22477,#22478,#22479,
#22480,#22481,#22482,#22483,#22484,#22485,#22486,#22487,#22488,#22489,#22490,
#22491,#22492,#22493,#22494,#22495,#22496,#22497,#22498,#22499,#22500,#22501,
#22502,#22503,#22504,#22505,#22506,#22507,#22508,#22509),.UNSPECIFIED.,
 .F.,.F.,(4,3,3,3,3,3,3,3,3,3,3,3,3,3,3,3,3,3,3,3,3,3,3,3,3,3,4),(0.,0.0183580651845695,
0.036716130369139,0.0506017132143072,0.0580120633809709,0.061133863191812,
0.078888287650872,0.0962814561595988,0.113365607257946,0.115724847189734,
0.119100212910273,0.135939557864133,0.147800793130485,0.16459229773457,
0.16938312183736,0.173083969688032,0.189885224893387,0.206611596082267,
0.216904963728089,0.222249975046034,0.226244647397093,0.242353326253545,
0.253193326851421,0.258082573110125,0.273549000401955,0.28213282996317,
0.286347380332243),.UNSPECIFIED.);
#225=B_SPLINE_CURVE_WITH_KNOTS('',3,(#22510,#22511,#22512,#22513,#22514,
#22515,#22516,#22517,#22518,#22519,#22520,#22521,#22522,#22523,#22524,#22525,
#22526,#22527,#22528,#22529,#22530,#22531,#22532,#22533,#22534,#22535,#22536,
#22537,#22538,#22539,#22540,#22541,#22542,#22543,#22544,#22545,#22546,#22547,
#22548,#22549,#22550,#22551,#22552,#22553,#22554,#22555,#22556,#22557,#22558,
#22559,#22560,#22561,#22562,#22563,#22564,#22565,#22566,#22567,#22568,#22569,
#22570,#22571,#22572,#22573,#22574,#22575,#22576,#22577,#22578,#22579,#22580,
#22581,#22582,#22583,#22584,#22585,#22586,#22587,#22588,#22589,#22590,#22591),
 .UNSPECIFIED.,.F.,.F.,(4,3,3,3,3,3,3,3,3,3,3,3,3,3,3,3,3,3,3,3,3,3,3,3,
3,3,3,4),(0.,0.0152191826672047,0.0310202687211212,0.04375636479767,0.0495387926916016,
0.0521713451608324,0.0684720803979817,0.0850884502494136,0.0971737854436662,
0.102033598682943,0.105097613961339,0.122175006430196,0.133459759972985,
0.150102685928275,0.154678331388736,0.158573680555885,0.175808037359126,
0.193042394162367,0.203920050772197,0.209203196649001,0.212511486881768,
0.215892595181776,0.233891080174088,0.246493248602607,0.251402765189765,
0.269591385970374,0.280063647041007,0.285110649527642),.UNSPECIFIED.);
#226=B_SPLINE_CURVE_WITH_KNOTS('',3,(#22592,#22593,#22594,#22595),
 .UNSPECIFIED.,.F.,.F.,(4,4),(-0.0158762351372481,0.),.UNSPECIFIED.);
#227=B_SPLINE_CURVE_WITH_KNOTS('',3,(#22692,#22693,#22694,#22695,#22696,
#22697,#22698,#22699,#22700,#22701,#22702,#22703,#22704,#22705,#22706,#22707,
#22708,#22709,#22710,#22711,#22712,#22713,#22714,#22715,#22716,#22717,#22718,
#22719,#22720,#22721,#22722,#22723,#22724,#22725,#22726,#22727,#22728,#22729,
#22730,#22731,#22732,#22733,#22734,#22735,#22736,#22737,#22738,#22739,#22740,
#22741,#22742,#22743,#22744,#22745,#22746,#22747,#22748,#22749,#22750,#22751,
#22752,#22753,#22754,#22755,#22756,#22757,#22758,#22759,#22760,#22761,#22762,
#22763,#22764,#22765,#22766,#22767,#22768,#22769,#22770,#22771,#22772,#22773),
 .UNSPECIFIED.,.F.,.F.,(4,3,3,3,3,3,3,3,3,3,3,3,3,3,3,3,3,3,3,3,3,3,3,3,
3,3,3,4),(0.,0.0151292672762648,0.0309291876229029,0.0437563608992012,0.0495387785849296,
0.0521713220847718,0.0686327765216655,0.0850784343717207,0.0971737657720376,
0.102033478715591,0.105097599596628,0.122174992255498,0.133459759972988,
0.150102687023667,0.15467833266872,0.158573680648776,0.175475135361472,
0.192932046543207,0.203920052454413,0.209203197488932,0.212511489653267,
0.215892595761394,0.233891634235224,0.246493249744474,0.251402765817797,
0.26959138653037,0.280063647041022,0.285131254558132),.UNSPECIFIED.);
#228=B_SPLINE_CURVE_WITH_KNOTS('',3,(#22774,#22775,#22776,#22777,#22778,
#22779,#22780,#22781,#22782,#22783,#22784,#22785,#22786,#22787,#22788,#22789,
#22790,#22791,#22792,#22793,#22794,#22795,#22796,#22797,#22798,#22799,#22800,
#22801,#22802,#22803,#22804,#22805,#22806,#22807,#22808,#22809,#22810,#22811,
#22812,#22813,#22814,#22815,#22816,#22817,#22818,#22819,#22820,#22821,#22822,
#22823,#22824,#22825,#22826,#22827,#22828,#22829,#22830,#22831,#22832,#22833,
#22834,#22835,#22836,#22837,#22838,#22839,#22840,#22841,#22842,#22843,#22844,
#22845,#22846,#22847,#22848,#22849,#22850,#22851,#22852),.UNSPECIFIED.,
 .F.,.F.,(4,3,3,3,3,3,3,3,3,3,3,3,3,3,3,3,3,3,3,3,3,3,3,3,3,3,4),(0.,0.0178407499527946,
0.0360809481309363,0.0506017130354889,0.0580120628747047,0.0611338628652755,
0.0788642583998809,0.0962814563820097,0.109161290569129,0.115724846961747,
0.119100212712732,0.135939558238763,0.147800793130486,0.164592297734572,
0.169383121808608,0.173083969711458,0.189885224767986,0.206611595947546,
0.2169049630076,0.222249974985313,0.226244647539912,0.242339285647356,0.253193327942412,
0.258082573330392,0.273549001447499,0.282132829963172,0.286347380332245),
 .UNSPECIFIED.);
#351=SHAPE_REPRESENTATION_RELATIONSHIP('SRR','None',#40772,#359);
#359=ADVANCED_BREP_SHAPE_REPRESENTATION('',(#377),#40732);
#368=STYLED_ITEM('',(#40815),#377);
#377=MANIFOLD_SOLID_BREP('Body1',#3173);
#389=FACE_BOUND('',#700,.T.);
#390=FACE_BOUND('',#708,.T.);
#417=PLANE('',#3415);
#418=PLANE('',#3416);
#419=PLANE('',#3417);
#420=PLANE('',#3418);
#421=PLANE('',#3419);
#422=PLANE('',#3420);
#423=PLANE('',#3421);
#424=PLANE('',#3422);
#521=FACE_OUTER_BOUND('',#689,.T.);
#522=FACE_OUTER_BOUND('',#690,.T.);
#523=FACE_OUTER_BOUND('',#691,.T.);
#524=FACE_OUTER_BOUND('',#692,.T.);
#525=FACE_OUTER_BOUND('',#693,.T.);
#526=FACE_OUTER_BOUND('',#694,.T.);
#527=FACE_OUTER_BOUND('',#695,.T.);
#528=FACE_OUTER_BOUND('',#696,.T.);
#529=FACE_OUTER_BOUND('',#697,.T.);
#530=FACE_OUTER_BOUND('',#698,.T.);
#531=FACE_OUTER_BOUND('',#699,.T.);
#532=FACE_OUTER_BOUND('',#701,.T.);
#533=FACE_OUTER_BOUND('',#702,.T.);
#534=FACE_OUTER_BOUND('',#703,.T.);
#535=FACE_OUTER_BOUND('',#704,.T.);
#536=FACE_OUTER_BOUND('',#705,.T.);
#537=FACE_OUTER_BOUND('',#706,.T.);
#538=FACE_OUTER_BOUND('',#707,.T.);
#689=EDGE_LOOP('',(#2452,#2453,#2454,#2455));
#690=EDGE_LOOP('',(#2456,#2457,#2458,#2459,#2460,#2461));
#691=EDGE_LOOP('',(#2462,#2463,#2464,#2465,#2466,#2467));
#692=EDGE_LOOP('',(#2468,#2469,#2470,#2471,#2472));
#693=EDGE_LOOP('',(#2473,#2474,#2475,#2476,#2477));
#694=EDGE_LOOP('',(#2478,#2479,#2480,#2481));
#695=EDGE_LOOP('',(#2482,#2483,#2484,#2485,#2486));
#696=EDGE_LOOP('',(#2487,#2488,#2489,#2490,#2491,#2492));
#697=EDGE_LOOP('',(#2493,#2494,#2495,#2496,#2497,#2498,#2499,#2500,#2501,
#2502,#2503,#2504,#2505,#2506));
#698=EDGE_LOOP('',(#2507,#2508,#2509,#2510,#2511,#2512,#2513,#2514,#2515,
#2516,#2517,#2518,#2519,#2520,#2521,#2522));
#699=EDGE_LOOP('',(#2523,#2524,#2525,#2526,#2527,#2528));
#700=EDGE_LOOP('',(#2529,#2530,#2531,#2532));
#701=EDGE_LOOP('',(#2533,#2534,#2535,#2536));
#702=EDGE_LOOP('',(#2537,#2538,#2539,#2540));
#703=EDGE_LOOP('',(#2541,#2542,#2543,#2544));
#704=EDGE_LOOP('',(#2545,#2546,#2547,#2548));
#705=EDGE_LOOP('',(#2549,#2550,#2551,#2552));
#706=EDGE_LOOP('',(#2553,#2554,#2555,#2556));
#707=EDGE_LOOP('',(#2557,#2558,#2559,#2560,#2561,#2562));
#708=EDGE_LOOP('',(#2563,#2564,#2565,#2566,#2567));
#833=LINE('',#20489,#975);
#834=LINE('',#20578,#976);
#835=LINE('',#20881,#977);
#836=LINE('',#21101,#978);
#837=LINE('',#21255,#979);
#838=LINE('',#21550,#980);
#839=LINE('',#22856,#981);
#840=LINE('',#22858,#982);
#841=LINE('',#22860,#983);
#842=LINE('',#22862,#984);
#843=LINE('',#22864,#985);
#844=LINE('',#22865,#986);
#845=LINE('',#22868,#987);
#846=LINE('',#22870,#988);
#847=LINE('',#22871,#989);
#848=LINE('',#22874,#990);
#849=LINE('',#22875,#991);
#850=LINE('',#22878,#992);
#851=LINE('',#22879,#993);
#852=LINE('',#22882,#994);
#853=LINE('',#22883,#995);
#854=LINE('',#22886,#996);
#855=LINE('',#22887,#997);
#856=LINE('',#22889,#998);
#975=VECTOR('',#3838,1.543);
#976=VECTOR('',#3843,1.543);
#977=VECTOR('',#3846,1.543);
#978=VECTOR('',#3851,1.2645);
#979=VECTOR('',#3856,1.2645);
#980=VECTOR('',#3859,1.2645);
#981=VECTOR('',#3868,10.);
#982=VECTOR('',#3869,9.99999999999999);
#983=VECTOR('',#3870,10.);
#984=VECTOR('',#3871,10.);
#985=VECTOR('',#3872,10.);
#986=VECTOR('',#3873,10.);
#987=VECTOR('',#3876,10.);
#988=VECTOR('',#3877,9.99999999999999);
#989=VECTOR('',#3878,10.);
#990=VECTOR('',#3881,10.);
#991=VECTOR('',#3882,10.);
#992=VECTOR('',#3885,10.);
#993=VECTOR('',#3886,10.);
#994=VECTOR('',#3889,10.);
#995=VECTOR('',#3890,10.);
#996=VECTOR('',#3893,10.);
#997=VECTOR('',#3894,10.);
#998=VECTOR('',#3897,10.);
#1082=CIRCLE('',#3404,1.543);
#1083=CIRCLE('',#3407,1.543);
#1084=CIRCLE('',#3409,1.2645);
#1085=CIRCLE('',#3412,1.2645);
#1279=VERTEX_POINT('',#20487);
#1280=VERTEX_POINT('',#20488);
#1281=VERTEX_POINT('',#20490);
#1282=VERTEX_POINT('',#20497);
#1283=VERTEX_POINT('',#20576);
#1284=VERTEX_POINT('',#20577);
#1285=VERTEX_POINT('',#20579);
#1286=VERTEX_POINT('',#20698);
#1287=VERTEX_POINT('',#20879);
#1288=VERTEX_POINT('',#20880);
#1289=VERTEX_POINT('',#20882);
#1290=VERTEX_POINT('',#20944);
#1291=VERTEX_POINT('',#20982);
#1292=VERTEX_POINT('',#20984);
#1293=VERTEX_POINT('',#21099);
#1294=VERTEX_POINT('',#21100);
#1295=VERTEX_POINT('',#21102);
#1296=VERTEX_POINT('',#21155);
#1297=VERTEX_POINT('',#21170);
#1298=VERTEX_POINT('',#21253);
#1299=VERTEX_POINT('',#21254);
#1300=VERTEX_POINT('',#21256);
#1301=VERTEX_POINT('',#21548);
#1302=VERTEX_POINT('',#21549);
#1303=VERTEX_POINT('',#21551);
#1304=VERTEX_POINT('',#21586);
#1305=VERTEX_POINT('',#21689);
#1306=VERTEX_POINT('',#21983);
#1307=VERTEX_POINT('',#22160);
#1308=VERTEX_POINT('',#22430);
#1309=VERTEX_POINT('',#22854);
#1310=VERTEX_POINT('',#22855);
#1311=VERTEX_POINT('',#22857);
#1312=VERTEX_POINT('',#22859);
#1313=VERTEX_POINT('',#22861);
#1314=VERTEX_POINT('',#22863);
#1315=VERTEX_POINT('',#22867);
#1316=VERTEX_POINT('',#22869);
#1317=VERTEX_POINT('',#22873);
#1318=VERTEX_POINT('',#22877);
#1319=VERTEX_POINT('',#22881);
#1320=VERTEX_POINT('',#22885);
#1702=EDGE_CURVE('',#1279,#1280,#833,.T.);
#1703=EDGE_CURVE('',#1280,#1281,#199,.T.);
#1704=EDGE_CURVE('',#1282,#1281,#1082,.T.);
#1705=EDGE_CURVE('',#1279,#1282,#200,.T.);
#1706=EDGE_CURVE('',#1283,#1284,#834,.T.);
#1707=EDGE_CURVE('',#1284,#1285,#201,.T.);
#1708=EDGE_CURVE('',#1285,#1280,#202,.T.);
#1709=EDGE_CURVE('',#1286,#1279,#203,.T.);
#1710=EDGE_CURVE('',#1283,#1286,#204,.T.);
#1711=EDGE_CURVE('',#1287,#1288,#835,.T.);
#1712=EDGE_CURVE('',#1289,#1287,#205,.T.);
#1713=EDGE_CURVE('',#1290,#1289,#206,.T.);
#1714=EDGE_CURVE('',#1291,#1290,#1083,.T.);
#1715=EDGE_CURVE('',#1291,#1292,#207,.T.);
#1716=EDGE_CURVE('',#1292,#1288,#208,.T.);
#1717=EDGE_CURVE('',#1293,#1294,#836,.T.);
#1718=EDGE_CURVE('',#1294,#1295,#209,.T.);
#1719=EDGE_CURVE('',#1295,#1296,#210,.T.);
#1720=EDGE_CURVE('',#1297,#1296,#1084,.T.);
#1721=EDGE_CURVE('',#1297,#1293,#211,.T.);
#1722=EDGE_CURVE('',#1298,#1299,#837,.T.);
#1723=EDGE_CURVE('',#1299,#1300,#212,.T.);
#1724=EDGE_CURVE('',#1300,#1294,#213,.T.);
#1725=EDGE_CURVE('',#1293,#1298,#214,.T.);
#1726=EDGE_CURVE('',#1301,#1302,#838,.T.);
#1727=EDGE_CURVE('',#1301,#1303,#215,.T.);
#1728=EDGE_CURVE('',#1304,#1303,#1085,.F.);
#1729=EDGE_CURVE('',#1304,#1302,#216,.T.);
#1730=EDGE_CURVE('',#1302,#1305,#217,.T.);
#1731=EDGE_CURVE('',#1305,#1299,#218,.T.);
#1732=EDGE_CURVE('',#1298,#1301,#219,.T.);
#1733=EDGE_CURVE('',#1288,#1306,#220,.T.);
#1734=EDGE_CURVE('',#1306,#1284,#221,.T.);
#1735=EDGE_CURVE('',#1307,#1283,#222,.T.);
#1736=EDGE_CURVE('',#1287,#1307,#223,.T.);
#1737=EDGE_CURVE('',#1281,#1308,#224,.T.);
#1738=EDGE_CURVE('',#1303,#1291,#225,.T.);
#1739=EDGE_CURVE('',#1308,#1297,#226,.T.);
#1740=EDGE_CURVE('',#1296,#1282,#227,.T.);
#1741=EDGE_CURVE('',#1290,#1304,#228,.T.);
#1742=EDGE_CURVE('',#1309,#1310,#839,.T.);
#1743=EDGE_CURVE('',#1310,#1311,#840,.T.);
#1744=EDGE_CURVE('',#1311,#1312,#841,.T.);
#1745=EDGE_CURVE('',#1312,#1313,#842,.T.);
#1746=EDGE_CURVE('',#1313,#1314,#843,.T.);
#1747=EDGE_CURVE('',#1314,#1309,#844,.T.);
#1748=EDGE_CURVE('',#1310,#1315,#845,.T.);
#1749=EDGE_CURVE('',#1316,#1315,#846,.T.);
#1750=EDGE_CURVE('',#1311,#1316,#847,.T.);
#1751=EDGE_CURVE('',#1317,#1316,#848,.T.);
#1752=EDGE_CURVE('',#1312,#1317,#849,.T.);
#1753=EDGE_CURVE('',#1318,#1317,#850,.T.);
#1754=EDGE_CURVE('',#1313,#1318,#851,.T.);
#1755=EDGE_CURVE('',#1319,#1318,#852,.T.);
#1756=EDGE_CURVE('',#1314,#1319,#853,.T.);
#1757=EDGE_CURVE('',#1320,#1319,#854,.T.);
#1758=EDGE_CURVE('',#1309,#1320,#855,.T.);
#1759=EDGE_CURVE('',#1315,#1320,#856,.T.);
#2452=ORIENTED_EDGE('',*,*,#1702,.T.);
#2453=ORIENTED_EDGE('',*,*,#1703,.T.);
#2454=ORIENTED_EDGE('',*,*,#1704,.F.);
#2455=ORIENTED_EDGE('',*,*,#1705,.F.);
#2456=ORIENTED_EDGE('',*,*,#1706,.T.);
#2457=ORIENTED_EDGE('',*,*,#1707,.T.);
#2458=ORIENTED_EDGE('',*,*,#1708,.T.);
#2459=ORIENTED_EDGE('',*,*,#1702,.F.);
#2460=ORIENTED_EDGE('',*,*,#1709,.F.);
#2461=ORIENTED_EDGE('',*,*,#1710,.F.);
#2462=ORIENTED_EDGE('',*,*,#1711,.F.);
#2463=ORIENTED_EDGE('',*,*,#1712,.F.);
#2464=ORIENTED_EDGE('',*,*,#1713,.F.);
#2465=ORIENTED_EDGE('',*,*,#1714,.F.);
#2466=ORIENTED_EDGE('',*,*,#1715,.T.);
#2467=ORIENTED_EDGE('',*,*,#1716,.T.);
#2468=ORIENTED_EDGE('',*,*,#1717,.T.);
#2469=ORIENTED_EDGE('',*,*,#1718,.T.);
#2470=ORIENTED_EDGE('',*,*,#1719,.T.);
#2471=ORIENTED_EDGE('',*,*,#1720,.F.);
#2472=ORIENTED_EDGE('',*,*,#1721,.T.);
#2473=ORIENTED_EDGE('',*,*,#1722,.T.);
#2474=ORIENTED_EDGE('',*,*,#1723,.T.);
#2475=ORIENTED_EDGE('',*,*,#1724,.T.);
#2476=ORIENTED_EDGE('',*,*,#1717,.F.);
#2477=ORIENTED_EDGE('',*,*,#1725,.T.);
#2478=ORIENTED_EDGE('',*,*,#1726,.F.);
#2479=ORIENTED_EDGE('',*,*,#1727,.T.);
#2480=ORIENTED_EDGE('',*,*,#1728,.F.);
#2481=ORIENTED_EDGE('',*,*,#1729,.T.);
#2482=ORIENTED_EDGE('',*,*,#1726,.T.);
#2483=ORIENTED_EDGE('',*,*,#1730,.T.);
#2484=ORIENTED_EDGE('',*,*,#1731,.T.);
#2485=ORIENTED_EDGE('',*,*,#1722,.F.);
#2486=ORIENTED_EDGE('',*,*,#1732,.T.);
#2487=ORIENTED_EDGE('',*,*,#1711,.T.);
#2488=ORIENTED_EDGE('',*,*,#1733,.T.);
#2489=ORIENTED_EDGE('',*,*,#1734,.T.);
#2490=ORIENTED_EDGE('',*,*,#1706,.F.);
#2491=ORIENTED_EDGE('',*,*,#1735,.F.);
#2492=ORIENTED_EDGE('',*,*,#1736,.F.);
#2493=ORIENTED_EDGE('',*,*,#1737,.F.);
#2494=ORIENTED_EDGE('',*,*,#1703,.F.);
#2495=ORIENTED_EDGE('',*,*,#1708,.F.);
#2496=ORIENTED_EDGE('',*,*,#1707,.F.);
#2497=ORIENTED_EDGE('',*,*,#1734,.F.);
#2498=ORIENTED_EDGE('',*,*,#1733,.F.);
#2499=ORIENTED_EDGE('',*,*,#1716,.F.);
#2500=ORIENTED_EDGE('',*,*,#1715,.F.);
#2501=ORIENTED_EDGE('',*,*,#1738,.F.);
#2502=ORIENTED_EDGE('',*,*,#1727,.F.);
#2503=ORIENTED_EDGE('',*,*,#1732,.F.);
#2504=ORIENTED_EDGE('',*,*,#1725,.F.);
#2505=ORIENTED_EDGE('',*,*,#1721,.F.);
#2506=ORIENTED_EDGE('',*,*,#1739,.F.);
#2507=ORIENTED_EDGE('',*,*,#1740,.F.);
#2508=ORIENTED_EDGE('',*,*,#1719,.F.);
#2509=ORIENTED_EDGE('',*,*,#1718,.F.);
#2510=ORIENTED_EDGE('',*,*,#1724,.F.);
#2511=ORIENTED_EDGE('',*,*,#1723,.F.);
#2512=ORIENTED_EDGE('',*,*,#1731,.F.);
#2513=ORIENTED_EDGE('',*,*,#1730,.F.);
#2514=ORIENTED_EDGE('',*,*,#1729,.F.);
#2515=ORIENTED_EDGE('',*,*,#1741,.F.);
#2516=ORIENTED_EDGE('',*,*,#1713,.T.);
#2517=ORIENTED_EDGE('',*,*,#1712,.T.);
#2518=ORIENTED_EDGE('',*,*,#1736,.T.);
#2519=ORIENTED_EDGE('',*,*,#1735,.T.);
#2520=ORIENTED_EDGE('',*,*,#1710,.T.);
#2521=ORIENTED_EDGE('',*,*,#1709,.T.);
#2522=ORIENTED_EDGE('',*,*,#1705,.T.);
#2523=ORIENTED_EDGE('',*,*,#1742,.T.);
#2524=ORIENTED_EDGE('',*,*,#1743,.T.);
#2525=ORIENTED_EDGE('',*,*,#1744,.T.);
#2526=ORIENTED_EDGE('',*,*,#1745,.T.);
#2527=ORIENTED_EDGE('',*,*,#1746,.T.);
#2528=ORIENTED_EDGE('',*,*,#1747,.T.);
#2529=ORIENTED_EDGE('',*,*,#1738,.T.);
#2530=ORIENTED_EDGE('',*,*,#1714,.T.);
#2531=ORIENTED_EDGE('',*,*,#1741,.T.);
#2532=ORIENTED_EDGE('',*,*,#1728,.T.);
#2533=ORIENTED_EDGE('',*,*,#1743,.F.);
#2534=ORIENTED_EDGE('',*,*,#1748,.T.);
#2535=ORIENTED_EDGE('',*,*,#1749,.F.);
#2536=ORIENTED_EDGE('',*,*,#1750,.F.);
#2537=ORIENTED_EDGE('',*,*,#1744,.F.);
#2538=ORIENTED_EDGE('',*,*,#1750,.T.);
#2539=ORIENTED_EDGE('',*,*,#1751,.F.);
#2540=ORIENTED_EDGE('',*,*,#1752,.F.);
#2541=ORIENTED_EDGE('',*,*,#1745,.F.);
#2542=ORIENTED_EDGE('',*,*,#1752,.T.);
#2543=ORIENTED_EDGE('',*,*,#1753,.F.);
#2544=ORIENTED_EDGE('',*,*,#1754,.F.);
#2545=ORIENTED_EDGE('',*,*,#1746,.F.);
#2546=ORIENTED_EDGE('',*,*,#1754,.T.);
#2547=ORIENTED_EDGE('',*,*,#1755,.F.);
#2548=ORIENTED_EDGE('',*,*,#1756,.F.);
#2549=ORIENTED_EDGE('',*,*,#1747,.F.);
#2550=ORIENTED_EDGE('',*,*,#1756,.T.);
#2551=ORIENTED_EDGE('',*,*,#1757,.F.);
#2552=ORIENTED_EDGE('',*,*,#1758,.F.);
#2553=ORIENTED_EDGE('',*,*,#1742,.F.);
#2554=ORIENTED_EDGE('',*,*,#1758,.T.);
#2555=ORIENTED_EDGE('',*,*,#1759,.F.);
#2556=ORIENTED_EDGE('',*,*,#1748,.F.);
#2557=ORIENTED_EDGE('',*,*,#1759,.T.);
#2558=ORIENTED_EDGE('',*,*,#1757,.T.);
#2559=ORIENTED_EDGE('',*,*,#1755,.T.);
#2560=ORIENTED_EDGE('',*,*,#1753,.T.);
#2561=ORIENTED_EDGE('',*,*,#1751,.T.);
#2562=ORIENTED_EDGE('',*,*,#1749,.T.);
#2563=ORIENTED_EDGE('',*,*,#1737,.T.);
#2564=ORIENTED_EDGE('',*,*,#1739,.T.);
#2565=ORIENTED_EDGE('',*,*,#1720,.T.);
#2566=ORIENTED_EDGE('',*,*,#1740,.T.);
#2567=ORIENTED_EDGE('',*,*,#1704,.T.);
#2954=CYLINDRICAL_SURFACE('',#3403,1.543);
#2955=CYLINDRICAL_SURFACE('',#3405,1.543);
#2956=CYLINDRICAL_SURFACE('',#3406,1.543);
#2957=CYLINDRICAL_SURFACE('',#3408,1.2645);
#2958=CYLINDRICAL_SURFACE('',#3410,1.2645);
#2959=CYLINDRICAL_SURFACE('',#3411,1.2645);
#2960=CYLINDRICAL_SURFACE('',#3413,1.2645);
#2961=CYLINDRICAL_SURFACE('',#3414,1.543);
#3100=ADVANCED_FACE('',(#521),#2954,.F.);
#3101=ADVANCED_FACE('',(#522),#2955,.F.);
#3102=ADVANCED_FACE('',(#523),#2956,.F.);
#3103=ADVANCED_FACE('',(#524),#2957,.F.);
#3104=ADVANCED_FACE('',(#525),#2958,.F.);
#3105=ADVANCED_FACE('',(#526),#2959,.F.);
#3106=ADVANCED_FACE('',(#527),#2960,.F.);
#3107=ADVANCED_FACE('',(#528),#2961,.F.);
#3108=ADVANCED_FACE('',(#529),#47,.F.);
#3109=ADVANCED_FACE('',(#530),#48,.F.);
#3110=ADVANCED_FACE('',(#531,#389),#417,.T.);
#3111=ADVANCED_FACE('',(#532),#418,.T.);
#3112=ADVANCED_FACE('',(#533),#419,.T.);
#3113=ADVANCED_FACE('',(#534),#420,.T.);
#3114=ADVANCED_FACE('',(#535),#421,.T.);
#3115=ADVANCED_FACE('',(#536),#422,.T.);
#3116=ADVANCED_FACE('',(#537),#423,.T.);
#3117=ADVANCED_FACE('',(#538,#390),#424,.F.);
#3173=CLOSED_SHELL('',(#3100,#3101,#3102,#3103,#3104,#3105,#3106,#3107,
#3108,#3109,#3110,#3111,#3112,#3113,#3114,#3115,#3116,#3117));
#3402=AXIS2_PLACEMENT_3D('',#20485,#3834,#3835);
#3403=AXIS2_PLACEMENT_3D('',#20486,#3836,#3837);
#3404=AXIS2_PLACEMENT_3D('',#20498,#3839,#3840);
#3405=AXIS2_PLACEMENT_3D('',#20575,#3841,#3842);
#3406=AXIS2_PLACEMENT_3D('',#20878,#3844,#3845);
#3407=AXIS2_PLACEMENT_3D('',#20983,#3847,#3848);
#3408=AXIS2_PLACEMENT_3D('',#21098,#3849,#3850);
#3409=AXIS2_PLACEMENT_3D('',#21171,#3852,#3853);
#3410=AXIS2_PLACEMENT_3D('',#21252,#3854,#3855);
#3411=AXIS2_PLACEMENT_3D('',#21547,#3857,#3858);
#3412=AXIS2_PLACEMENT_3D('',#21587,#3860,#3861);
#3413=AXIS2_PLACEMENT_3D('',#21688,#3862,#3863);
#3414=AXIS2_PLACEMENT_3D('',#21982,#3864,#3865);
#3415=AXIS2_PLACEMENT_3D('',#22853,#3866,#3867);
#3416=AXIS2_PLACEMENT_3D('',#22866,#3874,#3875);
#3417=AXIS2_PLACEMENT_3D('',#22872,#3879,#3880);
#3418=AXIS2_PLACEMENT_3D('',#22876,#3883,#3884);
#3419=AXIS2_PLACEMENT_3D('',#22880,#3887,#3888);
#3420=AXIS2_PLACEMENT_3D('',#22884,#3891,#3892);
#3421=AXIS2_PLACEMENT_3D('',#22888,#3895,#3896);
#3422=AXIS2_PLACEMENT_3D('',#22890,#3898,#3899);
#3834=DIRECTION('axis',(0.,0.,1.));
#3835=DIRECTION('refdir',(1.,0.,0.));
#3836=DIRECTION('center_axis',(-1.22464679914735E-16,1.22464679914735E-16,
1.));
#3837=DIRECTION('ref_axis',(0.609173230228443,-0.793037184231007,1.71721249579884E-16));
#3838=DIRECTION('',(-1.22464679914735E-16,1.22464679914735E-16,1.));
#3839=DIRECTION('center_axis',(1.22464679914735E-16,-1.22464679914735E-16,
-1.));
#3840=DIRECTION('ref_axis',(-1.,-4.24024356072764E-16,-1.22464679914735E-16));
#3841=DIRECTION('center_axis',(-1.22464679914735E-16,1.22464679914735E-16,
1.));
#3842=DIRECTION('ref_axis',(0.609173230228443,-0.793037184231007,1.71721249579884E-16));
#3843=DIRECTION('',(-1.22464679914735E-16,1.22464679914735E-16,1.));
#3844=DIRECTION('center_axis',(-1.22464679914735E-16,1.22464679914735E-16,
1.));
#3845=DIRECTION('ref_axis',(0.609173230228443,-0.793037184231007,1.71721249579884E-16));
#3846=DIRECTION('',(-1.22464679914735E-16,1.22464679914735E-16,1.));
#3847=DIRECTION('center_axis',(-1.22464679914735E-16,1.22464679914735E-16,
1.));
#3848=DIRECTION('ref_axis',(-1.,-4.24024356072764E-16,-1.22464679914735E-16));
#3849=DIRECTION('center_axis',(-1.22464679914735E-16,1.22464679914735E-16,
1.));
#3850=DIRECTION('ref_axis',(0.348694007966754,0.93723662370187,-7.20756830521819E-17));
#3851=DIRECTION('',(-1.22464679914735E-16,1.22464679914735E-16,1.));
#3852=DIRECTION('center_axis',(1.22464679914735E-16,-1.22464679914735E-16,
-1.));
#3853=DIRECTION('ref_axis',(-1.,1.258548236767E-48,-1.22464679914735E-16));
#3854=DIRECTION('center_axis',(-1.22464679914735E-16,1.22464679914735E-16,
1.));
#3855=DIRECTION('ref_axis',(0.348694007966754,0.93723662370187,-7.20756830521819E-17));
#3856=DIRECTION('',(-1.22464679914735E-16,1.22464679914735E-16,1.));
#3857=DIRECTION('center_axis',(-1.22464679914735E-16,1.22464679914735E-16,
1.));
#3858=DIRECTION('ref_axis',(0.348694007966754,0.93723662370187,-7.20756830521819E-17));
#3859=DIRECTION('',(-1.22464679914735E-16,1.22464679914735E-16,1.));
#3860=DIRECTION('center_axis',(1.22464679914735E-16,-1.22464679914735E-16,
-1.));
#3861=DIRECTION('ref_axis',(-1.,1.258548236767E-48,-1.22464679914735E-16));
#3862=DIRECTION('center_axis',(-1.22464679914735E-16,1.22464679914735E-16,
1.));
#3863=DIRECTION('ref_axis',(0.348694007966754,0.93723662370187,-7.20756830521819E-17));
#3864=DIRECTION('center_axis',(-1.22464679914735E-16,1.22464679914735E-16,
1.));
#3865=DIRECTION('ref_axis',(0.609173230228443,-0.793037184231007,1.71721249579884E-16));
#3866=DIRECTION('center_axis',(1.22464679914735E-16,-1.22464679914735E-16,
-1.));
#3867=DIRECTION('ref_axis',(-1.,1.258548236767E-48,-1.22464679914735E-16));
#3868=DIRECTION('',(-1.,-6.00925839494863E-16,-1.22464679914735E-16));
#3869=DIRECTION('',(-0.5,0.866025403784439,-1.67289863829858E-16));
#3870=DIRECTION('',(0.499999999999999,0.866025403784439,-4.48251839151231E-17));
#3871=DIRECTION('',(1.,7.21111007393836E-16,1.22464679914735E-16));
#3872=DIRECTION('',(0.500000000000001,-0.866025403784438,1.67289863829858E-16));
#3873=DIRECTION('',(-0.499999999999999,-0.866025403784439,4.48251839151232E-17));
#3874=DIRECTION('center_axis',(-0.866025403784438,-0.5,-4.48251839151229E-17));
#3875=DIRECTION('ref_axis',(0.5,-0.866025403784438,1.67289863829858E-16));
#3876=DIRECTION('',(-1.22464679914735E-16,1.22464679914735E-16,1.));
#3877=DIRECTION('',(0.5,-0.866025403784439,1.67289863829858E-16));
#3878=DIRECTION('',(-1.22464679914735E-16,1.22464679914735E-16,1.));
#3879=DIRECTION('center_axis',(-0.866025403784439,0.5,-1.67289863829858E-16));
#3880=DIRECTION('ref_axis',(-0.5,-0.866025403784439,4.4825183915123E-17));
#3881=DIRECTION('',(-0.499999999999999,-0.866025403784439,4.48251839151231E-17));
#3882=DIRECTION('',(-1.22464679914735E-16,1.22464679914735E-16,1.));
#3883=DIRECTION('center_axis',(-7.21111007393836E-16,1.,-1.22464679914735E-16));
#3884=DIRECTION('ref_axis',(-1.,-7.21111007393836E-16,-1.22464679914735E-16));
#3885=DIRECTION('',(-1.,-7.21111007393836E-16,-1.22464679914735E-16));
#3886=DIRECTION('',(-1.22464679914735E-16,1.22464679914735E-16,1.));
#3887=DIRECTION('center_axis',(0.866025403784438,0.500000000000001,4.48251839151229E-17));
#3888=DIRECTION('ref_axis',(-0.500000000000001,0.866025403784438,-1.67289863829858E-16));
#3889=DIRECTION('',(-0.500000000000001,0.866025403784438,-1.67289863829858E-16));
#3890=DIRECTION('',(-1.22464679914735E-16,1.22464679914735E-16,1.));
#3891=DIRECTION('center_axis',(0.866025403784439,-0.499999999999999,1.67289863829858E-16));
#3892=DIRECTION('ref_axis',(0.499999999999999,0.866025403784439,-4.48251839151232E-17));
#3893=DIRECTION('',(0.499999999999999,0.866025403784439,-4.48251839151232E-17));
#3894=DIRECTION('',(-1.22464679914735E-16,1.22464679914735E-16,1.));
#3895=DIRECTION('center_axis',(6.00925839494863E-16,-1.,1.22464679914735E-16));
#3896=DIRECTION('ref_axis',(1.,6.00925839494863E-16,1.22464679914735E-16));
#3897=DIRECTION('',(1.,6.00925839494863E-16,1.22464679914735E-16));
#3898=DIRECTION('center_axis',(1.22464679914735E-16,-1.22464679914735E-16,
-1.));
#3899=DIRECTION('ref_axis',(-1.,1.258548236767E-48,-1.22464679914735E-16));
#20485=CARTESIAN_POINT('',(0.,0.,0.));
#20486=CARTESIAN_POINT('Origin',(96.460480949577,-1.76391462320204E-15,
-7.60421172358872));
#20487=CARTESIAN_POINT('',(95.5205266553345,1.22365637526845,-5.21861757766303));
#20488=CARTESIAN_POINT('',(95.5203485097068,1.22389080463934,-5.17716043768798));
#20489=CARTESIAN_POINT('',(95.5205266553345,1.22365637526844,-7.60421172358872));
#20490=CARTESIAN_POINT('',(96.0619671077198,-1.49064942821852,-4.99999999999999));
#20491=CARTESIAN_POINT('Ctrl Pts',(95.5203485097069,1.22389080463943,-5.17716043768799));
#20492=CARTESIAN_POINT('Ctrl Pts',(95.4222725293664,1.15010481933258,-5.17083051560054));
#20493=CARTESIAN_POINT('Ctrl Pts',(94.9624927983586,0.710147272658132,-5.13813881494215));
#20494=CARTESIAN_POINT('Ctrl Pts',(94.7305471663323,-0.566638877030392,
-5.07908533571281));
#20495=CARTESIAN_POINT('Ctrl Pts',(95.5681568698448,-1.35863299878938,-5.02636177857093));
#20496=CARTESIAN_POINT('Ctrl Pts',(96.0619671077198,-1.49064942821852,-4.99999999999999));
#20497=CARTESIAN_POINT('',(96.8589954712671,-1.49064924647019,-5.0000135609018));
#20498=CARTESIAN_POINT('Origin',(96.460480949577,-1.44499066804254E-15,
-4.99999999999999));
#20499=CARTESIAN_POINT('Ctrl Pts',(95.5205266553345,1.22365637526844,-5.21861757766303));
#20500=CARTESIAN_POINT('Ctrl Pts',(95.4750144572141,1.18869608173482,-5.21565740437065));
#20501=CARTESIAN_POINT('Ctrl Pts',(95.4313991185652,1.15115000799943,-5.21269723107828));
#20502=CARTESIAN_POINT('Ctrl Pts',(95.3899849632427,1.11125485071705,-5.20973705778591));
#20503=CARTESIAN_POINT('Ctrl Pts',(95.3485989120151,1.07138676672107,-5.20677889329923));
#20504=CARTESIAN_POINT('Ctrl Pts',(95.3094114587368,1.0291731200483,-5.20382072881256));
#20505=CARTESIAN_POINT('Ctrl Pts',(95.2726926383603,0.984889804870097,-5.20086256432588));
#20506=CARTESIAN_POINT('Ctrl Pts',(95.2359845401275,0.940619420719128,-5.19790526364323));
#20507=CARTESIAN_POINT('Ctrl Pts',(95.2017439775786,0.894280968963252,-5.19494796296057));
#20508=CARTESIAN_POINT('Ctrl Pts',(95.1702014867204,0.846184322550652,-5.19199066227792));
#20509=CARTESIAN_POINT('Ctrl Pts',(95.1378112632144,0.79679503575649,-5.18895388149492));
#20510=CARTESIAN_POINT('Ctrl Pts',(95.1082666015211,0.745552129788192,-5.18591710071193));
#20511=CARTESIAN_POINT('Ctrl Pts',(95.0817688683063,0.692821764206503,-5.18288031992893));
#20512=CARTESIAN_POINT('Ctrl Pts',(95.0559329333177,0.64140837401016,-5.17991938473316));
#20513=CARTESIAN_POINT('Ctrl Pts',(95.0329936325855,0.58858149012942,-5.17695844953738));
#20514=CARTESIAN_POINT('Ctrl Pts',(95.0130891572679,0.534701785630407,-5.17399751434161));
#20515=CARTESIAN_POINT('Ctrl Pts',(94.9924198898227,0.478751854552561,-5.170922810765));
#20516=CARTESIAN_POINT('Ctrl Pts',(94.9750236328371,0.421667129375691,-5.1678481071884));
#20517=CARTESIAN_POINT('Ctrl Pts',(94.9609977142078,0.363866770737305,-5.16477340361179));
#20518=CARTESIAN_POINT('Ctrl Pts',(94.9469717955786,0.30606641209892,-5.16169870003519));
#20519=CARTESIAN_POINT('Ctrl Pts',(94.9363162543708,0.247551045391105,-5.15862399645858));
#20520=CARTESIAN_POINT('Ctrl Pts',(94.9290685719962,0.18874620470976,-5.15554929288198));
#20521=CARTESIAN_POINT('Ctrl Pts',(94.9220560770625,0.131849582307344,-5.15257436349912));
#20522=CARTESIAN_POINT('Ctrl Pts',(94.918204319441,0.0744450502569582,-5.14959943411625));
#20523=CARTESIAN_POINT('Ctrl Pts',(94.9175736512373,0.0169135664489606,
-5.14662450473339));
#20524=CARTESIAN_POINT('Ctrl Pts',(94.9169441008334,-0.0405159482364207,
-5.14365484813195));
#20525=CARTESIAN_POINT('Ctrl Pts',(94.9195243124124,-0.0980714527019945,
-5.14068519153051));
#20526=CARTESIAN_POINT('Ctrl Pts',(94.9253229143521,-0.155366685246577,
-5.13771553492907));
#20527=CARTESIAN_POINT('Ctrl Pts',(94.9311157645249,-0.212605085329118,
-5.13474882399848));
#20528=CARTESIAN_POINT('Ctrl Pts',(94.9401206269862,-0.269583210779604,
-5.13178211306788));
#20529=CARTESIAN_POINT('Ctrl Pts',(94.9522941165142,-0.325916364388086,
-5.12881540213729));
#20530=CARTESIAN_POINT('Ctrl Pts',(94.9644601768167,-0.382215139053537,
-5.1258505017282));
#20531=CARTESIAN_POINT('Ctrl Pts',(94.9797909208417,-0.437869215515292,
-5.12288560131911));
#20532=CARTESIAN_POINT('Ctrl Pts',(94.9981916392351,-0.492502764316785,
-5.11992070091002));
#20533=CARTESIAN_POINT('Ctrl Pts',(95.0165881500904,-0.54712382052268,-5.11695647845985));
#20534=CARTESIAN_POINT('Ctrl Pts',(95.038053075711,-0.600724320370488,-5.11399225600968));
#20535=CARTESIAN_POINT('Ctrl Pts',(95.0624421197003,-0.652944431140126,
-5.11102803355951));
#20536=CARTESIAN_POINT('Ctrl Pts',(95.0868523696764,-0.705209946681921,
-5.10806123375279));
#20537=CARTESIAN_POINT('Ctrl Pts',(95.114191599417,-0.756092202470218,-5.10509443394606));
#20538=CARTESIAN_POINT('Ctrl Pts',(95.144268246225,-0.805253450495386,-5.10212763413933));
#20539=CARTESIAN_POINT('Ctrl Pts',(95.1743571322149,-0.854434703857716,
-5.09915962704368));
#20540=CARTESIAN_POINT('Ctrl Pts',(95.2071853615618,-0.901893124030684,
-5.09619161994802));
#20541=CARTESIAN_POINT('Ctrl Pts',(95.2425182043213,-0.947320300199004,
-5.09322361285237));
#20542=CARTESIAN_POINT('Ctrl Pts',(95.2779171534899,-0.992832468891667,
-5.09025005272796));
#20543=CARTESIAN_POINT('Ctrl Pts',(95.3158297384057,-1.03630540574857,-5.08727649260356));
#20544=CARTESIAN_POINT('Ctrl Pts',(95.3559817788718,-1.07746488662573,-5.08430293247915));
#20545=CARTESIAN_POINT('Ctrl Pts',(95.3912650578024,-1.11363344562234,-5.08168994070915));
#20546=CARTESIAN_POINT('Ctrl Pts',(95.4282768703245,-1.1480159863261,-5.07907694893915));
#20547=CARTESIAN_POINT('Ctrl Pts',(95.4668104992014,-1.18045247089848,-5.07646395716915));
#20548=CARTESIAN_POINT('Ctrl Pts',(95.5103555387519,-1.21710741476826,-5.07351113820852));
#20549=CARTESIAN_POINT('Ctrl Pts',(95.5560263432748,-1.25142937469358,-5.07055831924789));
#20550=CARTESIAN_POINT('Ctrl Pts',(95.6035414147712,-1.28316157738879,-5.06760550028725));
#20551=CARTESIAN_POINT('Ctrl Pts',(95.6509741899481,-1.31483881976484,-5.06465779562247));
#20552=CARTESIAN_POINT('Ctrl Pts',(95.7002444587964,-1.34393491375805,-5.06171009095769));
#20553=CARTESIAN_POINT('Ctrl Pts',(95.7510378262279,-1.37023335776525,-5.05876238629291));
#20554=CARTESIAN_POINT('Ctrl Pts',(95.8017825605679,-1.39650662181891,-5.05581750396493));
#20555=CARTESIAN_POINT('Ctrl Pts',(95.8540470385658,-1.41998729947719,-5.05287262163696));
#20556=CARTESIAN_POINT('Ctrl Pts',(95.9074896665142,-1.44050325957859,-5.04992773930898));
#20557=CARTESIAN_POINT('Ctrl Pts',(95.9609023205119,-1.46100771305315,-5.04698450865424));
#20558=CARTESIAN_POINT('Ctrl Pts',(96.0154913228705,-1.47855055532387,-5.04404127799949));
#20559=CARTESIAN_POINT('Ctrl Pts',(96.0708944764094,-1.49300749493256,-5.04109804734474));
#20560=CARTESIAN_POINT('Ctrl Pts',(96.1262885285363,-1.50746205961214,-5.03815530019234));
#20561=CARTESIAN_POINT('Ctrl Pts',(96.1824959553726,-1.51883159556475,-5.03521255303994));
#20562=CARTESIAN_POINT('Ctrl Pts',(96.2391409909009,-1.52704211555977,-5.03226980588753));
#20563=CARTESIAN_POINT('Ctrl Pts',(96.2958391305459,-1.53526033282972,-5.02932429994105));
#20564=CARTESIAN_POINT('Ctrl Pts',(96.3529751744367,-1.54031354422022,-5.02637879399458));
#20565=CARTESIAN_POINT('Ctrl Pts',(96.4101662980206,-1.54217944346265,-5.0234332880481));
#20566=CARTESIAN_POINT('Ctrl Pts',(96.4673854787933,-1.54404625808991,-5.02048633707639));
#20567=CARTESIAN_POINT('Ctrl Pts',(96.5246592645381,-1.54272265947058,-5.01753938610469));
#20568=CARTESIAN_POINT('Ctrl Pts',(96.5816061911329,-1.5382384977168,-5.01459243513298));
#20569=CARTESIAN_POINT('Ctrl Pts',(96.6386579446969,-1.53374608159154,-5.01164005946222));
#20570=CARTESIAN_POINT('Ctrl Pts',(96.6953811140427,-1.52608155800054,-5.00868768379145));
#20571=CARTESIAN_POINT('Ctrl Pts',(96.7514019547242,-1.51532635717992,-5.00573530812069));
#20572=CARTESIAN_POINT('Ctrl Pts',(96.7875916908457,-1.50837844502977,-5.00382805904772));
#20573=CARTESIAN_POINT('Ctrl Pts',(96.8234885518963,-1.50014176996171,-5.00192080997476));
#20574=CARTESIAN_POINT('Ctrl Pts',(96.8589954712671,-1.49064924647019,-5.0000135609018));
#20575=CARTESIAN_POINT('Origin',(96.460480949577,-1.76391462320204E-15,
-7.60421172358872));
#20576=CARTESIAN_POINT('',(95.5205266553345,1.22365637526845,-5.71870242479901));
#20577=CARTESIAN_POINT('',(95.5205266553345,1.22365637526844,-5.67707251971253));
#20578=CARTESIAN_POINT('',(95.5205266553345,1.22365637526844,-7.60421172358872));
#20579=CARTESIAN_POINT('',(98.0032284820363,0.000204932544027349,-5.35421171129878));
#20580=CARTESIAN_POINT('Ctrl Pts',(95.5205266553345,1.22365637526844,-5.67707251971253));
#20581=CARTESIAN_POINT('Ctrl Pts',(95.4748841937922,1.18859601960518,-5.67411288279253));
#20582=CARTESIAN_POINT('Ctrl Pts',(95.431194703542,1.15096983641646,-5.67115324587254));
#20583=CARTESIAN_POINT('Ctrl Pts',(95.389751479782,1.11102988371714,-5.66819360895254));
#20584=CARTESIAN_POINT('Ctrl Pts',(95.3482719803909,1.07105497121361,-5.66523138143541));
#20585=CARTESIAN_POINT('Ctrl Pts',(95.3090430547088,1.02876260271372,-5.66226915391828));
#20586=CARTESIAN_POINT('Ctrl Pts',(95.2723218698293,0.98444248243012,-5.65930692640114));
#20587=CARTESIAN_POINT('Ctrl Pts',(95.235586418872,0.940105143903381,-5.65634354806688));
#20588=CARTESIAN_POINT('Ctrl Pts',(95.2013609632822,0.893738901946624,-5.65338016973261));
#20589=CARTESIAN_POINT('Ctrl Pts',(95.1698609586239,0.845664850252347,-5.65041679139835));
#20590=CARTESIAN_POINT('Ctrl Pts',(95.1382994660804,0.797496958198043,-5.64744762856122));
#20591=CARTESIAN_POINT('Ctrl Pts',(95.1094743206732,0.747615046009535,-5.64447846572409));
#20592=CARTESIAN_POINT('Ctrl Pts',(95.0835559073487,0.696366590298917,-5.64150930288695));
#20593=CARTESIAN_POINT('Ctrl Pts',(95.0578728079937,0.645583420691764,-5.63856709715883));
#20594=CARTESIAN_POINT('Ctrl Pts',(95.0350439730977,0.593458919368784,-5.63562489143071));
#20595=CARTESIAN_POINT('Ctrl Pts',(95.015187493322,0.54034787434249,-5.63268268570259));
#20596=CARTESIAN_POINT('Ctrl Pts',(94.9951440173245,0.486736661871289,-5.62971277207452));
#20597=CARTESIAN_POINT('Ctrl Pts',(94.9780457917068,0.431897056842871,-5.62674285844645));
#20598=CARTESIAN_POINT('Ctrl Pts',(94.9640403772373,0.376184281244761,-5.62377294481839));
#20599=CARTESIAN_POINT('Ctrl Pts',(94.9500597005158,0.320569911059979,-5.62080827694545));
#20600=CARTESIAN_POINT('Ctrl Pts',(94.9391611181184,0.264085933076503,-5.61784360907251));
#20601=CARTESIAN_POINT('Ctrl Pts',(94.9314431550967,0.207104860036487,-5.61487894119957));
#20602=CARTESIAN_POINT('Ctrl Pts',(94.9237328082311,0.15018001643842,-5.61191719888789));
#20603=CARTESIAN_POINT('Ctrl Pts',(94.9191969316952,0.0927595638259635,
-5.60895545657621));
#20604=CARTESIAN_POINT('Ctrl Pts',(94.9178831141031,0.0352266659123865,
-5.60599371426454));
#20605=CARTESIAN_POINT('Ctrl Pts',(94.9165700869607,-0.0222716177118651,
-5.60303375386563));
#20606=CARTESIAN_POINT('Ctrl Pts',(94.918475287831,-0.0798816922939508,
-5.60007379346672));
#20607=CARTESIAN_POINT('Ctrl Pts',(94.9235943283679,-0.137217030824841,
-5.59711383306781));
#20608=CARTESIAN_POINT('Ctrl Pts',(94.928712260639,-0.194539956328421,-5.59415451349653));
#20609=CARTESIAN_POINT('Ctrl Pts',(94.9370426047138,-0.251587744788432,
-5.59119519392525));
#20610=CARTESIAN_POINT('Ctrl Pts',(94.9485290217771,-0.307977869370634,
-5.58823587435398));
#20611=CARTESIAN_POINT('Ctrl Pts',(94.9600258197224,-0.364418956687777,
-5.58527388028925));
#20612=CARTESIAN_POINT('Ctrl Pts',(94.9746842868066,-0.420200680143225,
-5.58231188622452));
#20613=CARTESIAN_POINT('Ctrl Pts',(94.992396971953,-0.474950981306263,-5.57934989215979));
#20614=CARTESIAN_POINT('Ctrl Pts',(95.0101171507595,-0.529724445538065,
-5.57638664497187));
#20615=CARTESIAN_POINT('Ctrl Pts',(95.0308939360851,-0.583465129881837,
-5.57342339778395));
#20616=CARTESIAN_POINT('Ctrl Pts',(95.0545710783864,-0.635819498040814,
-5.57046015059603));
#20617=CARTESIAN_POINT('Ctrl Pts',(95.0782936927137,-0.68827441292784,-5.5674912124826));
#20618=CARTESIAN_POINT('Ctrl Pts',(95.1049275530735,-0.73933722734849,-5.56452227436917));
#20619=CARTESIAN_POINT('Ctrl Pts',(95.1342700994957,-0.788678503020507,
-5.56155333625574));
#20620=CARTESIAN_POINT('Ctrl Pts',(95.1604802446076,-0.832752455456761,
-5.55890134083375));
#20621=CARTESIAN_POINT('Ctrl Pts',(95.1888508426266,-0.875452974566531,
-5.55624934541176));
#20622=CARTESIAN_POINT('Ctrl Pts',(95.2192098937526,-0.916567054815212,
-5.55359734998977));
#20623=CARTESIAN_POINT('Ctrl Pts',(95.2532166176942,-0.962621036256481,
-5.5506267144506));
#20624=CARTESIAN_POINT('Ctrl Pts',(95.289860525436,-1.0068755466702,-5.54765607891144));
#20625=CARTESIAN_POINT('Ctrl Pts',(95.3289242373537,-1.049013063323,-5.54468544337228));
#20626=CARTESIAN_POINT('Ctrl Pts',(95.3679189255036,-1.09107612493763,-5.54172005680837));
#20627=CARTESIAN_POINT('Ctrl Pts',(95.4093245796525,-1.13102923844691,-5.53875467024447));
#20628=CARTESIAN_POINT('Ctrl Pts',(95.4528825877961,-1.16858655705792,-5.53578928368057));
#20629=CARTESIAN_POINT('Ctrl Pts',(95.4963975867957,-1.20610679160112,-5.5328268251371));
#20630=CARTESIAN_POINT('Ctrl Pts',(95.5420603362235,-1.24123557973104,-5.52986436659364));
#20631=CARTESIAN_POINT('Ctrl Pts',(95.5895755179663,-1.27372396114343,-5.52690190805017));
#20632=CARTESIAN_POINT('Ctrl Pts',(95.6370620606586,-1.30619276067987,-5.52394123508337));
#20633=CARTESIAN_POINT('Ctrl Pts',(95.6863983929707,-1.33602401481992,-5.52098056211656));
#20634=CARTESIAN_POINT('Ctrl Pts',(95.7372580288026,-1.36301049404125,-5.51801988914976));
#20635=CARTESIAN_POINT('Ctrl Pts',(95.7881065725598,-1.38999108772998,-5.51505986188176));
#20636=CARTESIAN_POINT('Ctrl Pts',(95.8404773000814,-1.41412789423585,-5.51209983461376));
#20637=CARTESIAN_POINT('Ctrl Pts',(95.894018740221,-1.43525940699636,-5.50913980734576));
#20638=CARTESIAN_POINT('Ctrl Pts',(95.9476083176209,-1.45640991837041,-5.50617711881943));
#20639=CARTESIAN_POINT('Ctrl Pts',(96.002370225348,-1.47454954419522,-5.50321443029311));
#20640=CARTESIAN_POINT('Ctrl Pts',(96.0579338846565,-1.48956532603436,-5.50025174176679));
#20641=CARTESIAN_POINT('Ctrl Pts',(96.1135209303122,-1.50458742790881,-5.49728780626603));
#20642=CARTESIAN_POINT('Ctrl Pts',(96.1699098895527,-1.51648295576778,-5.49432387076527));
#20643=CARTESIAN_POINT('Ctrl Pts',(96.2267190814007,-1.52518995177216,-5.49135993526452));
#20644=CARTESIAN_POINT('Ctrl Pts',(96.2836369827036,-1.53391360938986,-5.48839032800886));
#20645=CARTESIAN_POINT('Ctrl Pts',(96.3409762031023,-1.53943649198693,-5.4854207207532));
#20646=CARTESIAN_POINT('Ctrl Pts',(96.3983499902363,-1.54174859944526,-5.48245111349755));
#20647=CARTESIAN_POINT('Ctrl Pts',(96.4494786580482,-1.54380903470825,-5.47980474709068));
#20648=CARTESIAN_POINT('Ctrl Pts',(96.5006344931726,-1.54332039128355,-5.4771583806838));
#20649=CARTESIAN_POINT('Ctrl Pts',(96.5515469365361,-1.5403103537986,-5.47451201427693));
#20650=CARTESIAN_POINT('Ctrl Pts',(96.6086915661517,-1.5369318579763,-5.47154170646695));
#20651=CARTESIAN_POINT('Ctrl Pts',(96.6657666142044,-1.53036198970351,-5.46857139865697));
#20652=CARTESIAN_POINT('Ctrl Pts',(96.7223874348522,-1.52060974381029,-5.465601090847));
#20653=CARTESIAN_POINT('Ctrl Pts',(96.7789084359758,-1.51087469061287,-5.46263601953322));
#20654=CARTESIAN_POINT('Ctrl Pts',(96.8349762896129,-1.49796848339876,-5.45967094821944));
#20655=CARTESIAN_POINT('Ctrl Pts',(96.8902104071771,-1.48195195376596,-5.45670587690567));
#20656=CARTESIAN_POINT('Ctrl Pts',(96.9453901259224,-1.46595119844679,-5.45374372582279));
#20657=CARTESIAN_POINT('Ctrl Pts',(96.9997372373803,-1.44684633457203,-5.45078157473993));
#20658=CARTESIAN_POINT('Ctrl Pts',(97.0528820496656,-1.42474907847445,-5.44781942365706));
#20659=CARTESIAN_POINT('Ctrl Pts',(97.1059949740077,-1.40266508116957,-5.44485904992369));
#20660=CARTESIAN_POINT('Ctrl Pts',(97.1579065489178,-1.37759245067629,-5.44189867619032));
#20661=CARTESIAN_POINT('Ctrl Pts',(97.2082650614677,-1.34969178778116,-5.43893830245695));
#20662=CARTESIAN_POINT('Ctrl Pts',(97.2586127376763,-1.32179712865954,-5.43597856574836));
#20663=CARTESIAN_POINT('Ctrl Pts',(97.3074075593723,-1.29107589793588,-5.43301882903976));
#20664=CARTESIAN_POINT('Ctrl Pts',(97.3543225121326,-1.25773457495933,-5.43005909233116));
#20665=CARTESIAN_POINT('Ctrl Pts',(97.4012798979,-1.22436309587025,-5.42709667863961));
#20666=CARTESIAN_POINT('Ctrl Pts',(97.446353590799,-1.18836709109256,-5.42413426494806));
#20667=CARTESIAN_POINT('Ctrl Pts',(97.4892468475387,-1.14999553355268,-5.42117185125652));
#20668=CARTESIAN_POINT('Ctrl Pts',(97.532158277977,-1.11160771813977,-5.41820818240232));
#20669=CARTESIAN_POINT('Ctrl Pts',(97.5728870606587,-1.07084271222311,-5.41524451354813));
#20670=CARTESIAN_POINT('Ctrl Pts',(97.6111731483929,-1.02798660671445,-5.41228084469394));
#20671=CARTESIAN_POINT('Ctrl Pts',(97.6495327267123,-0.985048238418837,
-5.40931148704332));
#20672=CARTESIAN_POINT('Ctrl Pts',(97.6854399142855,-0.940011158372543,
-5.40634212939271));
#20673=CARTESIAN_POINT('Ctrl Pts',(97.7186754499643,-0.893194043416801,
-5.4033727717421));
#20674=CARTESIAN_POINT('Ctrl Pts',(97.7483218914283,-0.851432692811103,
-5.4007240740161));
#20675=CARTESIAN_POINT('Ctrl Pts',(97.7758430203872,-0.808255648373526,
-5.39807537629011));
#20676=CARTESIAN_POINT('Ctrl Pts',(97.8011141758143,-0.763905460582941,
-5.39542667856411));
#20677=CARTESIAN_POINT('Ctrl Pts',(97.8306220844796,-0.712119886536653,
-5.39233392204945));
#20678=CARTESIAN_POINT('Ctrl Pts',(97.8571762815607,-0.658533688473516,
-5.38924116553479));
#20679=CARTESIAN_POINT('Ctrl Pts',(97.8805635330969,-0.603501827655418,
-5.38614840902013));
#20680=CARTESIAN_POINT('Ctrl Pts',(97.9038863169094,-0.548621663961602,
-5.38306417778996));
#20681=CARTESIAN_POINT('Ctrl Pts',(97.9240593452705,-0.49230418697146,-5.37997994655978));
#20682=CARTESIAN_POINT('Ctrl Pts',(97.9409154985417,-0.434928208135278,
-5.37689571532961));
#20683=CARTESIAN_POINT('Ctrl Pts',(97.9577436590148,-0.377647512852836,
-5.37381660604277));
#20684=CARTESIAN_POINT('Ctrl Pts',(97.9712657552404,-0.319312245702585,
-5.37073749675593));
#20685=CARTESIAN_POINT('Ctrl Pts',(97.9813630912672,-0.260320016686897,
-5.36765838746908));
#20686=CARTESIAN_POINT('Ctrl Pts',(97.9914417164285,-0.201437103203514,
-5.36458498392478));
#20687=CARTESIAN_POINT('Ctrl Pts',(97.9981081279234,-0.14190010128785,-5.36151158038048));
#20688=CARTESIAN_POINT('Ctrl Pts',(98.0012942200649,-0.0821186062255512,
-5.35843817683618));
#20689=CARTESIAN_POINT('Ctrl Pts',(98.002754693151,-0.0547153608980888,
-5.35702935908703));
#20690=CARTESIAN_POINT('Ctrl Pts',(98.0034845801625,-0.0272608981217706,
-5.35562054133788));
#20691=CARTESIAN_POINT('Ctrl Pts',(98.0034809359953,0.000204726815253606,
-5.35421172358872));
#20692=CARTESIAN_POINT('Ctrl Pts',(98.001071826132,0.000206690037458163,
-5.35421160630865));
#20693=CARTESIAN_POINT('Ctrl Pts',(98.0013064289223,0.24592255753606,-5.3415881851562));
#20694=CARTESIAN_POINT('Ctrl Pts',(97.8302188552265,1.00442272708515,-5.30260298543279));
#20695=CARTESIAN_POINT('Ctrl Pts',(96.7594849884078,1.73376085900502,-5.24358592922591));
#20696=CARTESIAN_POINT('Ctrl Pts',(95.8307226241933,1.4573960907615,-5.19719229417148));
#20697=CARTESIAN_POINT('Ctrl Pts',(95.5203485097069,1.22389080463943,-5.17716043768799));
#20698=CARTESIAN_POINT('',(98.0034809091236,0.000353326024287275,-5.39578827645383));
#20699=CARTESIAN_POINT('Ctrl Pts',(98.0034809091234,0.000353326844981171,
-5.39578827641126));
#20700=CARTESIAN_POINT('Ctrl Pts',(98.003476520187,0.0195200805027758,-5.39479395094765));
#20701=CARTESIAN_POINT('Ctrl Pts',(98.0031150178881,0.0386823176935148,
-5.39379962548405));
#20702=CARTESIAN_POINT('Ctrl Pts',(98.0023968252469,0.0578310674047492,
-5.39280530002044));
#20703=CARTESIAN_POINT('Ctrl Pts',(98.000251161033,0.115039655516275,-5.38983466450877));
#20704=CARTESIAN_POINT('Ctrl Pts',(97.9949128750843,0.17224752489316,-5.38686402899711));
#20705=CARTESIAN_POINT('Ctrl Pts',(97.9863826482311,0.229069871533753,-5.38389339348544));
#20706=CARTESIAN_POINT('Ctrl Pts',(97.9778674938922,0.285791815729505,-5.38092800694861));
#20707=CARTESIAN_POINT('Ctrl Pts',(97.966171670182,0.342129078111066,-5.37796262041179));
#20708=CARTESIAN_POINT('Ctrl Pts',(97.9513477698711,0.397699791483852,-5.37499723387497));
#20709=CARTESIAN_POINT('Ctrl Pts',(97.9365385066668,0.453215634381072,-5.37203477535831));
#20710=CARTESIAN_POINT('Ctrl Pts',(97.9186074202501,0.507965926904492,-5.36907231684166));
#20711=CARTESIAN_POINT('Ctrl Pts',(97.8976582118212,0.561578593687674,-5.366109858325));
#20712=CARTESIAN_POINT('Ctrl Pts',(97.8767216302059,0.615158946259722,-5.3631491853847));
#20713=CARTESIAN_POINT('Ctrl Pts',(97.8527707220503,0.667602547953602,-5.36018851244439));
#20714=CARTESIAN_POINT('Ctrl Pts',(97.8259584511658,0.718554237796173,-5.35722783950409));
#20715=CARTESIAN_POINT('Ctrl Pts',(97.7991520278174,0.76949481549371,-5.35426781226224));
#20716=CARTESIAN_POINT('Ctrl Pts',(97.7694857233649,0.818943666434629,-5.35130778502038));
#20717=CARTESIAN_POINT('Ctrl Pts',(97.7371589055721,0.866569325949268,-5.34834775777853));
#20718=CARTESIAN_POINT('Ctrl Pts',(97.7048030238451,0.914237804062493,-5.34538506927761));
#20719=CARTESIAN_POINT('Ctrl Pts',(97.6697821416117,0.960079382567713,-5.34242238077668));
#20720=CARTESIAN_POINT('Ctrl Pts',(97.6323387667623,1.00379193875112,-5.33945969227576));
#20721=CARTESIAN_POINT('Ctrl Pts',(97.5948796322591,1.04752289324275,-5.33649575680003));
#20722=CARTESIAN_POINT('Ctrl Pts',(97.5549963330695,1.08912266127467,-5.3335318213243));
#20723=CARTESIAN_POINT('Ctrl Pts',(97.5129692854056,1.12832499881233,-5.33056788584858));
#20724=CARTESIAN_POINT('Ctrl Pts',(97.470861815224,1.1676023535319,-5.32759827861701));
#20725=CARTESIAN_POINT('Ctrl Pts',(97.4266028005723,1.20447277522765,-5.32462867138545));
#20726=CARTESIAN_POINT('Ctrl Pts',(97.3805061228808,1.23871008734385,-5.32165906415388));
#20727=CARTESIAN_POINT('Ctrl Pts',(97.3394270509994,1.26922068107591,-5.31901269753846));
#20728=CARTESIAN_POINT('Ctrl Pts',(97.2968892605857,1.29764065707482,-5.31636633092304));
#20729=CARTESIAN_POINT('Ctrl Pts',(97.2531318732976,1.32384044096142,-5.31371996430762));
#20730=CARTESIAN_POINT('Ctrl Pts',(97.2040181546192,1.35324733417394,-5.31074965658303));
#20731=CARTESIAN_POINT('Ctrl Pts',(97.1531637475995,1.37997846532703,-5.30777934885844));
#20732=CARTESIAN_POINT('Ctrl Pts',(97.1008914960143,1.40382453747323,-5.30480904113386));
#20733=CARTESIAN_POINT('Ctrl Pts',(97.0487113976704,1.42762857024337,-5.30184396990619));
#20734=CARTESIAN_POINT('Ctrl Pts',(96.9951188865058,1.44855742488113,-5.29887889867853));
#20735=CARTESIAN_POINT('Ctrl Pts',(96.9404626617286,1.46644691550702,-5.29591382745087));
#20736=CARTESIAN_POINT('Ctrl Pts',(96.8858602666252,1.48431878718006,-5.29295167645449));
#20737=CARTESIAN_POINT('Ctrl Pts',(96.8301967265524,1.49915706444531,-5.28998952545811));
#20738=CARTESIAN_POINT('Ctrl Pts',(96.7738404093114,1.5108457396422,-5.28702737446173));
#20739=CARTESIAN_POINT('Ctrl Pts',(96.7175179069856,1.52252740140064,-5.28406700081508));
#20740=CARTESIAN_POINT('Ctrl Pts',(96.6605039608838,1.53106310175209,-5.28110662716842));
#20741=CARTESIAN_POINT('Ctrl Pts',(96.6031796293305,1.53638734920482,-5.27814625352177));
#20742=CARTESIAN_POINT('Ctrl Pts',(96.5458676330524,1.54171045096503,-5.27518651689996));
#20743=CARTESIAN_POINT('Ctrl Pts',(96.4882459026943,1.54382342377984,-5.27222678027816));
#20744=CARTESIAN_POINT('Ctrl Pts',(96.4307009420754,1.54271259512367,-5.26926704365635));
#20745=CARTESIAN_POINT('Ctrl Pts',(96.3731039339497,1.54160076175984,-5.26630463005101));
#20746=CARTESIAN_POINT('Ctrl Pts',(96.3155843566986,1.53725930964672,-5.26334221644566));
#20747=CARTESIAN_POINT('Ctrl Pts',(96.2585276485382,1.52972672860205,-5.26037980284032));
#20748=CARTESIAN_POINT('Ctrl Pts',(96.2014467656781,1.52219095603283,-5.25741613407214));
#20749=CARTESIAN_POINT('Ctrl Pts',(96.1448296562402,1.51146145538865,-5.25445246530397));
#20750=CARTESIAN_POINT('Ctrl Pts',(96.0890523559733,1.49762805791478,-5.25148879653579));
#20751=CARTESIAN_POINT('Ctrl Pts',(96.0331679905079,1.48376810706812,-5.24851943896978));
#20752=CARTESIAN_POINT('Ctrl Pts',(95.9781271553534,1.46679250751296,-5.24555008140377));
#20753=CARTESIAN_POINT('Ctrl Pts',(95.9242905513001,1.44684099222951,-5.24258072383776));
#20754=CARTESIAN_POINT('Ctrl Pts',(95.8762677299935,1.42904402917615,-5.23993202542344));
#20755=CARTESIAN_POINT('Ctrl Pts',(95.8292030686934,1.40887998385358,-5.23728332700912));
#20756=CARTESIAN_POINT('Ctrl Pts',(95.7833362211146,1.38647899973839,-5.2346346285948));
#20757=CARTESIAN_POINT('Ctrl Pts',(95.7319583286611,1.36138646747434,-5.23166768080013));
#20758=CARTESIAN_POINT('Ctrl Pts',(95.6818691784263,1.33338154606915,-5.22870073300546));
#20759=CARTESIAN_POINT('Ctrl Pts',(95.6334196355374,1.30261989191745,-5.22573378521079));
#20760=CARTESIAN_POINT('Ctrl Pts',(95.5946843171056,1.27802600726951,-5.2233617160282));
#20761=CARTESIAN_POINT('Ctrl Pts',(95.5569968453978,1.25167103073437,-5.22098964684561));
#20762=CARTESIAN_POINT('Ctrl Pts',(95.5205266553345,1.22365637526844,-5.21861757766303));
#20763=CARTESIAN_POINT('Ctrl Pts',(95.5205266553345,1.22365637526844,-5.71870242479901));
#20764=CARTESIAN_POINT('Ctrl Pts',(95.4749536865538,1.18864940062048,-5.7157321319398));
#20765=CARTESIAN_POINT('Ctrl Pts',(95.4314109543683,1.15114839457577,-5.71276183908059));
#20766=CARTESIAN_POINT('Ctrl Pts',(95.3901664893481,1.11142969018513,-5.70979154622138));
#20767=CARTESIAN_POINT('Ctrl Pts',(95.387181520648,1.10855514473135,-5.70957657843817));
#20768=CARTESIAN_POINT('Ctrl Pts',(95.3842085724413,1.10566899796144,-5.70936161065496));
#20769=CARTESIAN_POINT('Ctrl Pts',(95.3812477380923,1.10277136126598,-5.70914664287175));
#20770=CARTESIAN_POINT('Ctrl Pts',(95.3403390789929,1.06273587876419,-5.7061765193443));
#20771=CARTESIAN_POINT('Ctrl Pts',(95.3015760537394,1.02033766352785,-5.70320639581685));
#20772=CARTESIAN_POINT('Ctrl Pts',(95.2652430743696,0.975835755478162,-5.7002362722894));
#20773=CARTESIAN_POINT('Ctrl Pts',(95.2289742695963,0.93141245072607,-5.69727139486294));
#20774=CARTESIAN_POINT('Ctrl Pts',(95.1951273183703,0.884893228937414,-5.69430651743647));
#20775=CARTESIAN_POINT('Ctrl Pts',(95.1639495713149,0.836573598185967,-5.69134164001001));
#20776=CARTESIAN_POINT('Ctrl Pts',(95.1328025923278,0.788301652140296,-5.68837968850217));
#20777=CARTESIAN_POINT('Ctrl Pts',(95.1043198796868,0.738233253343213,-5.68541773699433));
#20778=CARTESIAN_POINT('Ctrl Pts',(95.0787071842613,0.686695173628923,-5.6824557854865));
#20779=CARTESIAN_POINT('Ctrl Pts',(95.0531099036377,0.635188111707661,-5.67949561660617));
#20780=CARTESIAN_POINT('Ctrl Pts',(95.0303794476811,0.582213588207815,-5.67653544772585));
#20781=CARTESIAN_POINT('Ctrl Pts',(95.0106759326748,0.528123482686638,-5.67357527884552));
#20782=CARTESIAN_POINT('Ctrl Pts',(94.990976690292,0.47404510637522,-5.67061575186525));
#20783=CARTESIAN_POINT('Ctrl Pts',(94.9743032639424,0.418852117964194,-5.66765622488498));
#20784=CARTESIAN_POINT('Ctrl Pts',(94.9607670341548,0.362914827320599,-5.66469669790471));
#20785=CARTESIAN_POINT('Ctrl Pts',(94.9472185870789,0.306927049796871,-5.66173449976747));
#20786=CARTESIAN_POINT('Ctrl Pts',(94.9368131183915,0.250194135348607,-5.65877230163023));
#20787=CARTESIAN_POINT('Ctrl Pts',(94.9296112862886,0.193098612172937,-5.65581010349299));
#20788=CARTESIAN_POINT('Ctrl Pts',(94.9224064111878,0.135978964365221,-5.65284665373502));
#20789=CARTESIAN_POINT('Ctrl Pts',(94.9184079084876,0.0784969234628313,
-5.64988320397706));
#20790=CARTESIAN_POINT('Ctrl Pts',(94.9176243904604,0.0210389636377934,
-5.64691975421909));
#20791=CARTESIAN_POINT('Ctrl Pts',(94.9168393691463,-0.0365292371737625,
-5.6439506186758));
#20792=CARTESIAN_POINT('Ctrl Pts',(94.9192816368559,-0.0940727419538194,
-5.6409814831325));
#20793=CARTESIAN_POINT('Ctrl Pts',(94.9249076455712,-0.151207235358418,
-5.63801234758921));
#20794=CARTESIAN_POINT('Ctrl Pts',(94.9299296036579,-0.202207339642452,
-5.63536200077912));
#20795=CARTESIAN_POINT('Ctrl Pts',(94.9374875626971,-0.252881366441544,
-5.63271165396902));
#20796=CARTESIAN_POINT('Ctrl Pts',(94.9475163614128,-0.302963949936223,
-5.63006130715892));
#20797=CARTESIAN_POINT('Ctrl Pts',(94.9587555728084,-0.359091185021949,
-5.62709108022395));
#20798=CARTESIAN_POINT('Ctrl Pts',(94.9731456644885,-0.414708903174088,
-5.62412085328898));
#20799=CARTESIAN_POINT('Ctrl Pts',(94.990624657851,-0.469437409750782,-5.621150626354));
#20800=CARTESIAN_POINT('Ctrl Pts',(95.0080727808134,-0.524069257963947,
-5.61818564526425));
#20801=CARTESIAN_POINT('Ctrl Pts',(95.0285988198162,-0.577814519235535,
-5.6152206641745));
#20802=CARTESIAN_POINT('Ctrl Pts',(95.0520900154419,-0.630304669700307,
-5.61225568308475));
#20803=CARTESIAN_POINT('Ctrl Pts',(95.0755580300179,-0.682743023023606,
-5.60929362783049));
#20804=CARTESIAN_POINT('Ctrl Pts',(95.1019851919303,-0.733928246044934,
-5.60633157257623));
#20805=CARTESIAN_POINT('Ctrl Pts',(95.1312098473067,-0.783509627681161,
-5.60336951732197));
#20806=CARTESIAN_POINT('Ctrl Pts',(95.160416913738,-0.833061168616398,-5.60040924478941));
#20807=CARTESIAN_POINT('Ctrl Pts',(95.1924178718189,-0.881010333496331,
-5.59744897225685));
#20808=CARTESIAN_POINT('Ctrl Pts',(95.2270051316858,-0.927030963170926,
-5.59448869972429));
#20809=CARTESIAN_POINT('Ctrl Pts',(95.2615848885443,-0.973041609598184,
-5.59152906936315));
#20810=CARTESIAN_POINT('Ctrl Pts',(95.2987495201731,-1.0171241349703,-5.588569439002));
#20811=CARTESIAN_POINT('Ctrl Pts',(95.3382494053052,-1.05898317316256,-5.58560980864086));
#20812=CARTESIAN_POINT('Ctrl Pts',(95.3777849236423,-1.10087997277314,-5.5826475083703));
#20813=CARTESIAN_POINT('Ctrl Pts',(95.4196595471311,-1.14054889643074,-5.57968520809974));
#20814=CARTESIAN_POINT('Ctrl Pts',(95.4635857456885,-1.17773042436041,-5.57672290782919));
#20815=CARTESIAN_POINT('Ctrl Pts',(95.5075304960702,-1.214927655565,-5.57375935645847));
#20816=CARTESIAN_POINT('Ctrl Pts',(95.5535281325113,-1.24963508129856,-5.57079580508775));
#20817=CARTESIAN_POINT('Ctrl Pts',(95.6012594266263,-1.2816346493827,-5.56783225371703));
#20818=CARTESIAN_POINT('Ctrl Pts',(95.6490822614954,-1.31369558736362,-5.5648630187433));
#20819=CARTESIAN_POINT('Ctrl Pts',(95.6986449481703,-1.34303802339517,-5.56189378376956));
#20820=CARTESIAN_POINT('Ctrl Pts',(95.7496016140659,-1.36948879891122,-5.55892454879583));
#20821=CARTESIAN_POINT('Ctrl Pts',(95.795071575626,-1.3930915155492,-5.55627502301258));
#20822=CARTESIAN_POINT('Ctrl Pts',(95.8416509103096,-1.41439231708115,-5.55362549722934));
#20823=CARTESIAN_POINT('Ctrl Pts',(95.8890819197383,-1.43330113678159,-5.55097597144609));
#20824=CARTESIAN_POINT('Ctrl Pts',(95.9422538451485,-1.45449862683748,-5.54800575451384));
#20825=CARTESIAN_POINT('Ctrl Pts',(95.9967175171977,-1.47277737640127,-5.54503553758159));
#20826=CARTESIAN_POINT('Ctrl Pts',(96.0521208977492,-1.48798221362729,-5.54206532064933));
#20827=CARTESIAN_POINT('Ctrl Pts',(96.10742645343,-1.50316020391331,-5.53910034818202));
#20828=CARTESIAN_POINT('Ctrl Pts',(96.1636679256365,-1.51527491800201,-5.53613537571471));
#20829=CARTESIAN_POINT('Ctrl Pts',(96.2204749385166,-1.5242198380335,-5.5331704032474));
#20830=CARTESIAN_POINT('Ctrl Pts',(96.2772259103806,-1.53315593376,-5.53020835577229));
#20831=CARTESIAN_POINT('Ctrl Pts',(96.3345408051066,-1.53892835047816,-5.52724630829718));
#20832=CARTESIAN_POINT('Ctrl Pts',(96.3920375051383,-1.54148126648149,-5.52428426082207));
#20833=CARTESIAN_POINT('Ctrl Pts',(96.4494996169699,-1.54403264673112,-5.52132399522124));
#20834=CARTESIAN_POINT('Ctrl Pts',(96.5071427975625,-1.543368342504,-5.51836372962041));
#20835=CARTESIAN_POINT('Ctrl Pts',(96.5645804497071,-1.53948442475806,-5.51540346401958));
#20836=CARTESIAN_POINT('Ctrl Pts',(96.6220056584249,-1.53560134843313,-5.51244383973759));
#20837=CARTESIAN_POINT('Ctrl Pts',(96.679224907255,-1.52850007866818,-5.5094842154556));
#20838=CARTESIAN_POINT('Ctrl Pts',(96.7358544800438,-1.5182287109386,-5.5065245911736));
#20839=CARTESIAN_POINT('Ctrl Pts',(96.7925351651291,-1.50794807255469,-5.50356229561605));
#20840=CARTESIAN_POINT('Ctrl Pts',(96.848624596372,-1.49449171112577,-5.50060000005849));
#20841=CARTESIAN_POINT('Ctrl Pts',(96.9037484226053,-1.47795904792898,-5.49763770450093));
#20842=CARTESIAN_POINT('Ctrl Pts',(96.9588955437214,-1.46141939816253,-5.49467415710125));
#20843=CARTESIAN_POINT('Ctrl Pts',(97.0130757548387,-1.44180103184701,-5.49171060970156));
#20844=CARTESIAN_POINT('Ctrl Pts',(97.0659321690558,-1.41925255709888,-5.48874706230188));
#20845=CARTESIAN_POINT('Ctrl Pts',(97.1188899761845,-1.39666082827187,-5.48577783001599));
#20846=CARTESIAN_POINT('Ctrl Pts',(97.1705184429738,-1.37112799073345,-5.4828085977301));
#20847=CARTESIAN_POINT('Ctrl Pts',(97.2204837749586,-1.34284947235793,-5.47983936544422));
#20848=CARTESIAN_POINT('Ctrl Pts',(97.2650700384127,-1.31761530658144,-5.4771897888739));
#20849=CARTESIAN_POINT('Ctrl Pts',(97.3083321370077,-1.29019560379683,-5.47454021230359));
#20850=CARTESIAN_POINT('Ctrl Pts',(97.3500540021067,-1.26075722651627,-5.47189063573328));
#20851=CARTESIAN_POINT('Ctrl Pts',(97.396541183261,-1.22795650741416,-5.46893843439439));
#20852=CARTESIAN_POINT('Ctrl Pts',(97.4413143141274,-1.19250873107517,-5.4659862330555));
#20853=CARTESIAN_POINT('Ctrl Pts',(97.4840534865511,-1.15462039716629,-5.46303403171661));
#20854=CARTESIAN_POINT('Ctrl Pts',(97.5267172034443,-1.11679895468675,-5.46008704245614));
#20855=CARTESIAN_POINT('Ctrl Pts',(97.5673536947163,-1.07654585136958,-5.45714005319566));
#20856=CARTESIAN_POINT('Ctrl Pts',(97.605673592613,-1.03410967036203,-5.45419306393519));
#20857=CARTESIAN_POINT('Ctrl Pts',(97.6439560356009,-0.991714967630169,
-5.45124895514204));
#20858=CARTESIAN_POINT('Ctrl Pts',(97.6799260173105,-0.947141803429666,
-5.4483048463489));
#20859=CARTESIAN_POINT('Ctrl Pts',(97.7133301206631,-0.90067638722735,-5.44536073755575));
#20860=CARTESIAN_POINT('Ctrl Pts',(97.7467148424364,-0.854237930980674,
-5.44241833698022));
#20861=CARTESIAN_POINT('Ctrl Pts',(97.777536328314,-0.805909826724527,-5.43947593640469));
#20862=CARTESIAN_POINT('Ctrl Pts',(97.805582153967,-0.75601041656096,-5.43653353582916));
#20863=CARTESIAN_POINT('Ctrl Pts',(97.8336228464436,-0.706120139395519,
-5.43359167379585));
#20864=CARTESIAN_POINT('Ctrl Pts',(97.8588886290636,-0.654659588043249,
-5.43064981176254));
#20865=CARTESIAN_POINT('Ctrl Pts',(97.8812122520137,-0.60197306108882,-5.42770794972922));
#20866=CARTESIAN_POINT('Ctrl Pts',(97.9035559399446,-0.549239178283588,
-5.42476344348329));
#20867=CARTESIAN_POINT('Ctrl Pts',(97.9229519806668,-0.495277606861794,
-5.42181893723735));
#20868=CARTESIAN_POINT('Ctrl Pts',(97.9392813010349,-0.440452631423638,
-5.41887443099142));
#20869=CARTESIAN_POINT('Ctrl Pts',(97.9556183951784,-0.385601555876467,
-5.41592852297679));
#20870=CARTESIAN_POINT('Ctrl Pts',(97.9688857392088,-0.329886772435975,
-5.41298261496217));
#20871=CARTESIAN_POINT('Ctrl Pts',(97.9790150338574,-0.273684553599324,
-5.41003670694755));
#20872=CARTESIAN_POINT('Ctrl Pts',(97.9891624434043,-0.217381824557753,
-5.40708553056764));
#20873=CARTESIAN_POINT('Ctrl Pts',(97.9961605356595,-0.160590444823081,
-5.40413435418774));
#20874=CARTESIAN_POINT('Ctrl Pts',(97.9999928529454,-0.103692330415918,
-5.40118317780784));
#20875=CARTESIAN_POINT('Ctrl Pts',(98.0023280769435,-0.0690214427267606,
-5.39938487735651));
#20876=CARTESIAN_POINT('Ctrl Pts',(98.0034888467739,-0.0343109594795624,
-5.39758657690517));
#20877=CARTESIAN_POINT('Ctrl Pts',(98.0034809091236,0.000353326024288114,
-5.39578827645384));
#20878=CARTESIAN_POINT('Origin',(96.460480949577,-1.76391462320204E-15,
-7.60421172358872));
#20879=CARTESIAN_POINT('',(95.5205266553345,1.22365637526844,-6.21868058178697));
#20880=CARTESIAN_POINT('',(95.5205266553345,1.22365637526844,-6.17704955921195));
#20881=CARTESIAN_POINT('',(95.5205266553345,1.22365637526844,-7.60421172358872));
#20882=CARTESIAN_POINT('',(98.0034803814948,-0.00132404739565839,-6.39578827645092));
#20883=CARTESIAN_POINT('Ctrl Pts',(98.0034803814954,-0.0013240466246711,
-6.39578827641126));
#20884=CARTESIAN_POINT('Ctrl Pts',(98.0035294092285,0.0558112255743518,
-6.39284931489647));
#20885=CARTESIAN_POINT('Ctrl Pts',(98.000400664574,0.112996196184301,-6.38991035338168));
#20886=CARTESIAN_POINT('Ctrl Pts',(97.9941042309439,0.169848847065066,-6.38697139186689));
#20887=CARTESIAN_POINT('Ctrl Pts',(97.9878096391193,0.226684867654557,-6.3840332900444));
#20888=CARTESIAN_POINT('Ctrl Pts',(97.9783492542707,0.283188235566044,-6.3810951882219));
#20889=CARTESIAN_POINT('Ctrl Pts',(97.9657850465216,0.338981674610642,-6.37815708639941));
#20890=CARTESIAN_POINT('Ctrl Pts',(97.9528393442749,0.396469202962078,-6.37512977324732));
#20891=CARTESIAN_POINT('Ctrl Pts',(97.9365983367856,0.453202398648983,-6.37210246009523));
#20892=CARTESIAN_POINT('Ctrl Pts',(97.9171860160137,0.508782221994395,-6.36907514694314));
#20893=CARTESIAN_POINT('Ctrl Pts',(97.8983213792134,0.562793959857088,-6.36613324402663));
#20894=CARTESIAN_POINT('Ctrl Pts',(97.8764623091867,0.61571607736221,-6.36319134111012));
#20895=CARTESIAN_POINT('Ctrl Pts',(97.8517715838318,0.667202646154045,-6.36024943819362));
#20896=CARTESIAN_POINT('Ctrl Pts',(97.8260056153116,0.720931375935481,-6.35717941992374));
#20897=CARTESIAN_POINT('Ctrl Pts',(97.7971559708585,0.773096069312216,-6.35410940165386));
#20898=CARTESIAN_POINT('Ctrl Pts',(97.7654592242794,0.823335109511779,-6.35103938338398));
#20899=CARTESIAN_POINT('Ctrl Pts',(97.7337624777003,0.873574149711343,-6.3479693651141));
#20900=CARTESIAN_POINT('Ctrl Pts',(97.6992190724388,0.92188706063909,-6.34489934684422));
#20901=CARTESIAN_POINT('Ctrl Pts',(97.662112314353,0.967951994257261,-6.34182932857434));
#20902=CARTESIAN_POINT('Ctrl Pts',(97.6262157705618,1.01251454814676,-6.33885943707885));
#20903=CARTESIAN_POINT('Ctrl Pts',(97.5877611235107,1.0551717064333,-6.33588954558335));
#20904=CARTESIAN_POINT('Ctrl Pts',(97.5469782282762,1.09561519858899,-6.33291965408785));
#20905=CARTESIAN_POINT('Ctrl Pts',(97.5062689650265,1.13598567153943,-6.32995512461984));
#20906=CARTESIAN_POINT('Ctrl Pts',(97.4632401644032,1.17415004716957,-6.32699059515184));
#20907=CARTESIAN_POINT('Ctrl Pts',(97.4181615998277,1.20983336544144,-6.32402606568383));
#20908=CARTESIAN_POINT('Ctrl Pts',(97.3731285950243,1.24548061948056,-6.32106453239123));
#20909=CARTESIAN_POINT('Ctrl Pts',(97.3260503376017,1.27865146231512,-6.31810299909863));
#20910=CARTESIAN_POINT('Ctrl Pts',(97.2772317951421,1.30910926063057,-6.31514146580603));
#20911=CARTESIAN_POINT('Ctrl Pts',(97.22844377863,1.3395480138638,-6.31218178434279));
#20912=CARTESIAN_POINT('Ctrl Pts',(97.1779180757227,1.36727680997693,-6.30922210287954));
#20913=CARTESIAN_POINT('Ctrl Pts',(97.1259891167632,1.39210196444385,-6.3062624214163));
#20914=CARTESIAN_POINT('Ctrl Pts',(97.0740726173981,1.41692116247797,-6.30330345008535));
#20915=CARTESIAN_POINT('Ctrl Pts',(97.0207540006523,1.43883787713433,-6.30034447875439));
#20916=CARTESIAN_POINT('Ctrl Pts',(96.9663908171012,1.45770511625006,-6.29738550742343));
#20917=CARTESIAN_POINT('Ctrl Pts',(96.9119804370647,1.47658873533691,-6.29442396720232));
#20918=CARTESIAN_POINT('Ctrl Pts',(96.856524171388,1.4924174156804,-6.2914624269812));
#20919=CARTESIAN_POINT('Ctrl Pts',(96.8003966884087,1.5050934490903,-6.28850088676009));
#20920=CARTESIAN_POINT('Ctrl Pts',(96.7442465679591,1.5177745950282,-6.28553815208351));
#20921=CARTESIAN_POINT('Ctrl Pts',(96.6874252056233,1.52730047099368,-6.28257541740693));
#20922=CARTESIAN_POINT('Ctrl Pts',(96.6303162990154,1.53362477616956,-6.27961268273036));
#20923=CARTESIAN_POINT('Ctrl Pts',(96.5730994693102,1.53996103287181,-6.27664434914598));
#20924=CARTESIAN_POINT('Ctrl Pts',(96.5155945319472,1.54308359937165,-6.2736760155616));
#20925=CARTESIAN_POINT('Ctrl Pts',(96.4581881356583,1.54299829650079,-6.27070768197723));
#20926=CARTESIAN_POINT('Ctrl Pts',(96.4068499374961,1.54292201065162,-6.26805311893866));
#20927=CARTESIAN_POINT('Ctrl Pts',(96.3555908081535,1.54028094513122,-6.26539855590009));
#20928=CARTESIAN_POINT('Ctrl Pts',(96.304682680796,1.53511429523826,-6.26274399286152));
#20929=CARTESIAN_POINT('Ctrl Pts',(96.2476427768939,1.52932533326523,-6.259769693305));
#20930=CARTESIAN_POINT('Ctrl Pts',(96.1908111694043,1.52034130012038,-6.25679539374849));
#20931=CARTESIAN_POINT('Ctrl Pts',(96.134572654946,1.50818857689968,-6.25382109419198));
#20932=CARTESIAN_POINT('Ctrl Pts',(96.0784269630212,1.49605591193566,-6.25085170376265));
#20933=CARTESIAN_POINT('Ctrl Pts',(96.0228729253038,1.48076504427997,-6.24788231333332));
#20934=CARTESIAN_POINT('Ctrl Pts',(95.9682890204752,1.46239396365242,-6.24491292290399));
#20935=CARTESIAN_POINT('Ctrl Pts',(95.9137589250248,1.44404099342626,-6.24194645973047));
#20936=CARTESIAN_POINT('Ctrl Pts',(95.8601975568746,1.42261399382697,-6.23897999655696));
#20937=CARTESIAN_POINT('Ctrl Pts',(95.8079701860178,1.39824128942019,-6.23601353338344));
#20938=CARTESIAN_POINT('Ctrl Pts',(95.7557619845293,1.37387753069333,-6.23304815901114));
#20939=CARTESIAN_POINT('Ctrl Pts',(95.704887285087,1.34657041820749,-6.23008278463884));
#20940=CARTESIAN_POINT('Ctrl Pts',(95.6556914329275,1.31649642380486,-6.22711741026653));
#20941=CARTESIAN_POINT('Ctrl Pts',(95.6090354951532,1.28797510849305,-6.22430513410668));
#20942=CARTESIAN_POINT('Ctrl Pts',(95.5638897013052,1.25696579292471,-6.22149285794683));
#20943=CARTESIAN_POINT('Ctrl Pts',(95.5205266553345,1.22365637526844,-6.21868058178697));
#20944=CARTESIAN_POINT('',(96.8589947914343,-1.49064942821851,-6.49999999999999));
#20945=CARTESIAN_POINT('Ctrl Pts',(96.8589947914343,-1.4906494282185,-6.49999999999999));
#20946=CARTESIAN_POINT('Ctrl Pts',(96.915764516961,-1.47547247179094,-6.49696938050472));
#20947=CARTESIAN_POINT('Ctrl Pts',(96.9717164672414,-1.45703484475423,-6.49393876100945));
#20948=CARTESIAN_POINT('Ctrl Pts',(97.0264642179596,-1.43544834108058,-6.49090814151418));
#20949=CARTESIAN_POINT('Ctrl Pts',(97.0811796713535,-1.41387457192662,-6.48787930987136));
#20950=CARTESIAN_POINT('Ctrl Pts',(97.1346918794132,-1.38915579118626,-6.48485047822855));
#20951=CARTESIAN_POINT('Ctrl Pts',(97.1866316757174,-1.36145294554228,-6.48182164658573));
#20952=CARTESIAN_POINT('Ctrl Pts',(97.2385557247662,-1.33375849892596,-6.47879373323272));
#20953=CARTESIAN_POINT('Ctrl Pts',(97.2889078761591,-1.30308201422557,-6.47576581987971));
#20954=CARTESIAN_POINT('Ctrl Pts',(97.3373426670593,-1.26963086305194,-6.4727379065267));
#20955=CARTESIAN_POINT('Ctrl Pts',(97.3857779905807,-1.23617934402719,-6.46970995987674));
#20956=CARTESIAN_POINT('Ctrl Pts',(97.432295508573,-1.19995337703009,-6.46668201322678));
#20957=CARTESIAN_POINT('Ctrl Pts',(97.4765794454682,-1.16120318921698,-6.46365406657682));
#20958=CARTESIAN_POINT('Ctrl Pts',(97.5208777825532,-1.12244040067102,-6.46062513530333));
#20959=CARTESIAN_POINT('Ctrl Pts',(97.5629407278518,-1.08115208480294,-6.45759620402984));
#20960=CARTESIAN_POINT('Ctrl Pts',(97.6024876336847,-1.03762697220795,-6.45456727275634));
#20961=CARTESIAN_POINT('Ctrl Pts',(97.6420930678142,-0.994037443683377,
-6.45153385875065));
#20962=CARTESIAN_POINT('Ctrl Pts',(97.6791746980187,-0.948204873361764,
-6.44850044474496));
#20963=CARTESIAN_POINT('Ctrl Pts',(97.7134912103065,-0.900452267755797,
-6.44546703073927));
#20964=CARTESIAN_POINT('Ctrl Pts',(97.7478340052991,-0.852663088863378,
-6.44243129346937));
#20965=CARTESIAN_POINT('Ctrl Pts',(97.7794072000822,-0.802951359379204,
-6.43939555619948));
#20966=CARTESIAN_POINT('Ctrl Pts',(97.8080137200766,-0.751667767321239,
-6.43635981892958));
#20967=CARTESIAN_POINT('Ctrl Pts',(97.8366807930495,-0.700275620491613,
-6.43331765574931));
#20968=CARTESIAN_POINT('Ctrl Pts',(97.8623684296765,-0.64730540536536,-6.43027549256904));
#20969=CARTESIAN_POINT('Ctrl Pts',(97.8849265505216,-0.59313044935296,-6.42723332938877));
#20970=CARTESIAN_POINT('Ctrl Pts',(97.9005445173536,-0.555622774314743,
-6.42512710768823));
#20971=CARTESIAN_POINT('Ctrl Pts',(97.9146633972451,-0.51753805012281,-6.4230208859877));
#20972=CARTESIAN_POINT('Ctrl Pts',(97.9272474852871,-0.479004101987811,
-6.42091466428717));
#20973=CARTESIAN_POINT('Ctrl Pts',(97.9479486403942,-0.415614745955782,
-6.41744987431055));
#20974=CARTESIAN_POINT('Ctrl Pts',(97.9645639136385,-0.350798124206962,
-6.41398508433394));
#20975=CARTESIAN_POINT('Ctrl Pts',(97.9769231303583,-0.285047561553121,
-6.41052029435732));
#20976=CARTESIAN_POINT('Ctrl Pts',(97.9891473600444,-0.220015124781231,
-6.40709334672391));
#20977=CARTESIAN_POINT('Ctrl Pts',(97.9972078859358,-0.154069184982509,
-6.4036663990905));
#20978=CARTESIAN_POINT('Ctrl Pts',(98.0009861219586,-0.0877086875140339,
-6.40023945145709));
#20979=CARTESIAN_POINT('Ctrl Pts',(98.0026219401416,-0.0589773674661508,
-6.39875572645503));
#20980=CARTESIAN_POINT('Ctrl Pts',(98.0034556299914,-0.0301686006272956,
-6.39727200145298));
#20981=CARTESIAN_POINT('Ctrl Pts',(98.0034803814948,-0.00132404739565834,
-6.39578827645092));
#20982=CARTESIAN_POINT('',(96.0617145053845,-1.49058187396268,-6.49999996996503));
#20983=CARTESIAN_POINT('Origin',(96.460480949577,-1.62868768791465E-15,
-6.49999999999999));
#20984=CARTESIAN_POINT('',(98.0034806316228,0.000990558803381491,-6.35421172362388));
#20985=CARTESIAN_POINT('Ctrl Pts',(96.0617145053845,-1.49058187396268,-6.49999996996503));
#20986=CARTESIAN_POINT('Ctrl Pts',(96.116690584544,-1.50528929526237,-6.49704678467027));
#20987=CARTESIAN_POINT('Ctrl Pts',(96.1726030058333,-1.51698360757519,-6.49409359937551));
#20988=CARTESIAN_POINT('Ctrl Pts',(96.229088163052,-1.5255511719848,-6.49114041408075));
#20989=CARTESIAN_POINT('Ctrl Pts',(96.2854728766418,-1.53410350129014,-6.48819248023013));
#20990=CARTESIAN_POINT('Ctrl Pts',(96.3424277877649,-1.53954003633601,-6.48524454637951));
#20991=CARTESIAN_POINT('Ctrl Pts',(96.3995765076143,-1.54179753824853,-6.48229661252888));
#20992=CARTESIAN_POINT('Ctrl Pts',(96.4566688759794,-1.54405281415171,-6.47935158548787));
#20993=CARTESIAN_POINT('Ctrl Pts',(96.5139541496305,-1.54313524452192,-6.47640655844686));
#20994=CARTESIAN_POINT('Ctrl Pts',(96.5710500339397,-1.53903329320168,-6.47346153140585));
#20995=CARTESIAN_POINT('Ctrl Pts',(96.6281122636852,-1.53493375973315,-6.4705182402798));
#20996=CARTESIAN_POINT('Ctrl Pts',(96.6849847996598,-1.52765360202188,-6.46757494915375));
#20997=CARTESIAN_POINT('Ctrl Pts',(96.7412868843653,-1.51723334625485,-6.46463165802771));
#20998=CARTESIAN_POINT('Ctrl Pts',(96.7975781110642,-1.50681510006181,-6.46168893452317));
#20999=CARTESIAN_POINT('Ctrl Pts',(96.8532985860008,-1.49325805459338,-6.45874621101863));
#21000=CARTESIAN_POINT('Ctrl Pts',(96.9080765059447,-1.47665406169484,-6.45580348751409));
#21001=CARTESIAN_POINT('Ctrl Pts',(96.962903420947,-1.46003521767378,-6.45285813194704));
#21002=CARTESIAN_POINT('Ctrl Pts',(97.0167855908051,-1.44036413669594,-6.44991277637998));
#21003=CARTESIAN_POINT('Ctrl Pts',(97.0693666645714,-1.41778248898616,-6.44696742081293));
#21004=CARTESIAN_POINT('Ctrl Pts',(97.1219722445091,-1.39519031677222,-6.44402069252023));
#21005=CARTESIAN_POINT('Ctrl Pts',(97.1732750471856,-1.36968511148393,-6.44107396422753));
#21006=CARTESIAN_POINT('Ctrl Pts',(97.2229419852295,-1.34145524305203,-6.43812723593483));
#21007=CARTESIAN_POINT('Ctrl Pts',(97.2726985259559,-1.31317444593322,-6.43517519153508));
#21008=CARTESIAN_POINT('Ctrl Pts',(97.3208128653744,-1.28215945799747,-6.43222314713533));
#21009=CARTESIAN_POINT('Ctrl Pts',(97.3669807123812,-1.2486421344949,-6.42927110273557));
#21010=CARTESIAN_POINT('Ctrl Pts',(97.3968781136849,-1.22693696658367,-6.42735941610066));
#21011=CARTESIAN_POINT('Ctrl Pts',(97.4259598757987,-1.2041832735016,-6.42544772946574));
#21012=CARTESIAN_POINT('Ctrl Pts',(97.4541514013328,-1.18045246973672,-6.42353604283083));
#21013=CARTESIAN_POINT('Ctrl Pts',(97.497390358046,-1.14405517738296,-6.42060397959229));
#21014=CARTESIAN_POINT('Ctrl Pts',(97.5387259925091,-1.10519533681692,-6.41767191635376));
#21015=CARTESIAN_POINT('Ctrl Pts',(97.577859829369,-1.06410217507283,-6.41473985311523));
#21016=CARTESIAN_POINT('Ctrl Pts',(97.6169405909014,-1.02306474599376,-6.41181176649206));
#21017=CARTESIAN_POINT('Ctrl Pts',(97.6538250987265,-0.979800374259077,
-6.4088836798689));
#21018=CARTESIAN_POINT('Ctrl Pts',(97.6882484389171,-0.934577975408972,
-6.40595559324573));
#21019=CARTESIAN_POINT('Ctrl Pts',(97.7226391559366,-0.889398434051653,
-6.40303028158485));
#21020=CARTESIAN_POINT('Ctrl Pts',(97.7545730006852,-0.842264963907663,
-6.40010496992396));
#21021=CARTESIAN_POINT('Ctrl Pts',(97.7838240659667,-0.793480936320484,
-6.39717965826308));
#21022=CARTESIAN_POINT('Ctrl Pts',(97.8130593554045,-0.744723219200589,
-6.39425592429721));
#21023=CARTESIAN_POINT('Ctrl Pts',(97.8396144577919,-0.69431716737565,-6.39133219033133));
#21024=CARTESIAN_POINT('Ctrl Pts',(97.8633070811437,-0.642594619175778,
-6.38840845636546));
#21025=CARTESIAN_POINT('Ctrl Pts',(97.8870109123206,-0.590847603559806,
-6.38548333932357));
#21026=CARTESIAN_POINT('Ctrl Pts',(97.9078493244683,-0.537783329902571,
-6.38255822228169));
#21027=CARTESIAN_POINT('Ctrl Pts',(97.9256870770652,-0.483756141016263,
-6.37963310523981));
#21028=CARTESIAN_POINT('Ctrl Pts',(97.9435281104811,-0.429719015147953,
-6.37670745019408));
#21029=CARTESIAN_POINT('Ctrl Pts',(97.9583672355104,-0.374719136651115,
-6.37378179514835));
#21030=CARTESIAN_POINT('Ctrl Pts',(97.9701192774561,-0.319125553659244,
-6.37085614010262));
#21031=CARTESIAN_POINT('Ctrl Pts',(97.9818901361726,-0.26344295705512,-6.36792580064712));
#21032=CARTESIAN_POINT('Ctrl Pts',(97.9905639489311,-0.207165286916391,
-6.36499546119161));
#21033=CARTESIAN_POINT('Ctrl Pts',(97.9961070578707,-0.150670021991439,
-6.3620651217361));
#21034=CARTESIAN_POINT('Ctrl Pts',(98.0010589575786,-0.100200350741447,
-6.35944732236536));
#21035=CARTESIAN_POINT('Ctrl Pts',(98.0035130818555,-0.0495573729400543,
-6.35682952299462));
#21036=CARTESIAN_POINT('Ctrl Pts',(98.0034806316228,0.000990558803380336,
-6.35421172362388));
#21037=CARTESIAN_POINT('Ctrl Pts',(98.0034806316223,0.000990559482311531,
-6.35421172358872));
#21038=CARTESIAN_POINT('Ctrl Pts',(98.0034402990849,0.0638167637889655,
-6.35095805143181));
#21039=CARTESIAN_POINT('Ctrl Pts',(97.9995628740167,0.126518520347403,-6.34770437927491));
#21040=CARTESIAN_POINT('Ctrl Pts',(97.9918933276673,0.188746200575634,-6.34445070711801));
#21041=CARTESIAN_POINT('Ctrl Pts',(97.984897247495,0.245509641329849,-6.34148274131831));
#21042=CARTESIAN_POINT('Ctrl Pts',(97.9747261260543,0.302003370910422,-6.33851477551861));
#21043=CARTESIAN_POINT('Ctrl Pts',(97.9614127380147,0.357844612167181,-6.33554680971891));
#21044=CARTESIAN_POINT('Ctrl Pts',(97.9481230811933,0.413586315975266,-6.33258413434143));
#21045=CARTESIAN_POINT('Ctrl Pts',(97.9317023948098,0.468677336106132,-6.32962145896395));
#21046=CARTESIAN_POINT('Ctrl Pts',(97.9122349375888,0.522742152778854,-6.32665878358647));
#21047=CARTESIAN_POINT('Ctrl Pts',(97.8927868733996,0.576753111328393,-6.32369905955785));
#21048=CARTESIAN_POINT('Ctrl Pts',(97.8702982275636,0.629739402907963,-6.32073933552924));
#21049=CARTESIAN_POINT('Ctrl Pts',(97.844903368191,0.681339538584773,-6.31777961150063));
#21050=CARTESIAN_POINT('Ctrl Pts',(97.8195239884064,0.732908221091223,-6.31482169158944));
#21051=CARTESIAN_POINT('Ctrl Pts',(97.7912421366924,0.783091954952207,-6.31186377167826));
#21052=CARTESIAN_POINT('Ctrl Pts',(97.7602398503536,0.831550238922453,-6.30890585176707));
#21053=CARTESIAN_POINT('Ctrl Pts',(97.7292444761241,0.879997718884657,-6.30594859133839));
#21054=CARTESIAN_POINT('Ctrl Pts',(97.6955301527396,0.92672007303637,-6.30299133090971));
#21055=CARTESIAN_POINT('Ctrl Pts',(97.6593231617635,0.971404318643746,-6.30003407048103));
#21056=CARTESIAN_POINT('Ctrl Pts',(97.6230835810073,1.01612878437716,-6.29707414823306));
#21057=CARTESIAN_POINT('Ctrl Pts',(97.5843471780464,1.05881106844031,-6.29411422598508));
#21058=CARTESIAN_POINT('Ctrl Pts',(97.5433807445106,1.09917106681933,-6.2911543037371));
#21059=CARTESIAN_POINT('Ctrl Pts',(97.5023971101579,1.13954801138771,-6.2881931386892));
#21060=CARTESIAN_POINT('Ctrl Pts',(97.4591819707229,1.17760037988561,-6.2852319736413));
#21061=CARTESIAN_POINT('Ctrl Pts',(97.4140368499147,1.21308703106216,-6.2822708085934));
#21062=CARTESIAN_POINT('Ctrl Pts',(97.3688048204051,1.24864199745671,-6.27930394301787));
#21063=CARTESIAN_POINT('Ctrl Pts',(97.32163581439,1.28162107604611,-6.27633707744233));
#21064=CARTESIAN_POINT('Ctrl Pts',(97.2728613021965,1.3118258888579,-6.27337021186679));
#21065=CARTESIAN_POINT('Ctrl Pts',(97.2289954580633,1.33899088859419,-6.27070193171292));
#21066=CARTESIAN_POINT('Ctrl Pts',(97.1838316157734,1.36391240691739,-6.26803365155905));
#21067=CARTESIAN_POINT('Ctrl Pts',(97.1376256759733,1.38647900074749,-6.26536537140518));
#21068=CARTESIAN_POINT('Ctrl Pts',(97.0861889261889,1.41160027834394,-6.26239502475228));
#21069=CARTESIAN_POINT('Ctrl Pts',(97.0332453252879,1.43390757435751,-6.25942467809939));
#21070=CARTESIAN_POINT('Ctrl Pts',(96.9791343172436,1.45321976459452,-6.25645433144649));
#21071=CARTESIAN_POINT('Ctrl Pts',(96.9251189641295,1.47249781563735,-6.25348923563464));
#21072=CARTESIAN_POINT('Ctrl Pts',(96.8699407869667,1.48879109626221,-6.25052413982279));
#21073=CARTESIAN_POINT('Ctrl Pts',(96.8139611609895,1.50196562548541,-6.24755904401093));
#21074=CARTESIAN_POINT('Ctrl Pts',(96.7580368325766,1.51512714069926,-6.24459687716785));
#21075=CARTESIAN_POINT('Ctrl Pts',(96.7013131288064,1.52517588971202,-6.24163471032476));
#21076=CARTESIAN_POINT('Ctrl Pts',(96.6441669333127,1.53202756482351,-6.23867254348168));
#21077=CARTESIAN_POINT('Ctrl Pts',(96.5870551945963,1.53887510866009,-6.23571216270191));
#21078=CARTESIAN_POINT('Ctrl Pts',(96.5295219856489,1.54252933805977,-6.23275178192214));
#21079=CARTESIAN_POINT('Ctrl Pts',(96.4719525472493,1.542957356004,-6.22979140114237));
#21080=CARTESIAN_POINT('Ctrl Pts',(96.4143956660283,1.54338528058796,-6.22683166608768));
#21081=CARTESIAN_POINT('Ctrl Pts',(96.3568030920146,1.540588387079,-6.22387193103298));
#21082=CARTESIAN_POINT('Ctrl Pts',(96.299561093711,1.53458587247116,-6.22091219597828));
#21083=CARTESIAN_POINT('Ctrl Pts',(96.2422675842191,1.52857795629333,-6.21794979750382));
#21084=CARTESIAN_POINT('Ctrl Pts',(96.1853258005499,1.5193587082637,-6.21498739902936));
#21085=CARTESIAN_POINT('Ctrl Pts',(96.1291165203249,1.50699920870132,-6.2120250005549));
#21086=CARTESIAN_POINT('Ctrl Pts',(96.072883566014,1.49463450359544,-6.20906135438476));
#21087=CARTESIAN_POINT('Ctrl Pts',(96.0173842335257,1.47912704977739,-6.20609770821463));
#21088=CARTESIAN_POINT('Ctrl Pts',(95.9629855749006,1.46059828569512,-6.20313406204449));
#21089=CARTESIAN_POINT('Ctrl Pts',(95.9084827210883,1.44203403161937,-6.20016473930668));
#21090=CARTESIAN_POINT('Ctrl Pts',(95.855085238972,1.42043709890194,-6.19719541656887));
#21091=CARTESIAN_POINT('Ctrl Pts',(95.8031406644171,1.39597734562772,-6.19422609383106));
#21092=CARTESIAN_POINT('Ctrl Pts',(95.756805226356,1.37415883248101,-6.19157740778482));
#21093=CARTESIAN_POINT('Ctrl Pts',(95.7116257642638,1.35006318764398,-6.18892872173859));
#21094=CARTESIAN_POINT('Ctrl Pts',(95.6678300253879,1.32384044068091,-6.18628003569235));
#21095=CARTESIAN_POINT('Ctrl Pts',(95.6169550468038,1.29337899113337,-6.18320321019889));
#21096=CARTESIAN_POINT('Ctrl Pts',(95.5677292674599,1.25991516398024,-6.18012638470542));
#21097=CARTESIAN_POINT('Ctrl Pts',(95.5205266553345,1.22365637526844,-6.17704955921195));
#21098=CARTESIAN_POINT('Origin',(96.460480949577,-1.62868768791465E-15,
-6.49999999999999));
#21099=CARTESIAN_POINT('',(96.0195573809006,-1.18513571230711,-5.34780246104806));
#21100=CARTESIAN_POINT('',(96.0195573765031,-1.18513571067102,-5.20989040793544));
#21101=CARTESIAN_POINT('',(96.0195573765031,-1.18513571067102,-6.49999999999999));
#21102=CARTESIAN_POINT('',(97.7249794730849,-0.00193236804568257,-5.05658136948322));
#21103=CARTESIAN_POINT('Ctrl Pts',(96.019557376503,-1.18513571067102,-5.20989040793544));
#21104=CARTESIAN_POINT('Ctrl Pts',(96.0659867832952,-1.20240952982453,-5.20677992089892));
#21105=CARTESIAN_POINT('Ctrl Pts',(96.1134623860598,-1.21696187683096,-5.20366943386241));
#21106=CARTESIAN_POINT('Ctrl Pts',(96.1616345923433,-1.22867860108661,-5.20055894682589));
#21107=CARTESIAN_POINT('Ctrl Pts',(96.2097989355969,-1.24039341285038,-5.19744896750647));
#21108=CARTESIAN_POINT('Ctrl Pts',(96.2586591240462,-1.24927339216687,-5.19433898818704));
#21109=CARTESIAN_POINT('Ctrl Pts',(96.3078529130282,-1.25525492727942,-5.19122900886762));
#21110=CARTESIAN_POINT('Ctrl Pts',(96.3570953780928,-1.2612423809785,-5.18811595229773));
#21111=CARTESIAN_POINT('Ctrl Pts',(96.4066715574073,-1.26432559872759,-5.18500289572785));
#21112=CARTESIAN_POINT('Ctrl Pts',(96.4562133814324,-1.26449279865966,-5.18188983915796));
#21113=CARTESIAN_POINT('Ctrl Pts',(96.5057819011462,-1.26466008868767,-5.17877510511271));
#21114=CARTESIAN_POINT('Ctrl Pts',(96.5553154807588,-1.2619082622699,-5.17566037106747));
#21115=CARTESIAN_POINT('Ctrl Pts',(96.6044489378048,-1.25627762392141,-5.17254563702222));
#21116=CARTESIAN_POINT('Ctrl Pts',(96.6536755227132,-1.25063631322573,-5.16942499929055));
#21117=CARTESIAN_POINT('Ctrl Pts',(96.7024999308461,-1.24210539354816,-5.16630436155888));
#21118=CARTESIAN_POINT('Ctrl Pts',(96.7505665543627,-1.23077641832143,-5.16318372382721));
#21119=CARTESIAN_POINT('Ctrl Pts',(96.7763049368317,-1.22471005717443,-5.16151270636002));
#21120=CARTESIAN_POINT('Ctrl Pts',(96.801826286488,-1.21784226493739,-5.15984168889283));
#21121=CARTESIAN_POINT('Ctrl Pts',(96.8270781716263,-1.21019284694042,-5.15817067142564));
#21122=CARTESIAN_POINT('Ctrl Pts',(96.8739312376288,-1.19599989919293,-5.15507021808312));
#21123=CARTESIAN_POINT('Ctrl Pts',(96.9200694895639,-1.17904840191129,-5.15196976474061));
#21124=CARTESIAN_POINT('Ctrl Pts',(96.9651428358136,-1.15942944182909,-5.1488693113981));
#21125=CARTESIAN_POINT('Ctrl Pts',(97.0101340164064,-1.13984624578211,-5.145774509972));
#21126=CARTESIAN_POINT('Ctrl Pts',(97.0540636334913,-1.11760544580946,-5.1426797085459));
#21127=CARTESIAN_POINT('Ctrl Pts',(97.0965975601529,-1.09284761414818,-5.13958490711981));
#21128=CARTESIAN_POINT('Ctrl Pts',(97.1390890137287,-1.06811450490481,-5.13649319606832));
#21129=CARTESIAN_POINT('Ctrl Pts',(97.1801870556191,-1.04086961515804,-5.13340148501682));
#21130=CARTESIAN_POINT('Ctrl Pts',(97.2195804340792,-1.0113002633385,-5.13030977396533));
#21131=CARTESIAN_POINT('Ctrl Pts',(97.2589518291673,-0.981747412618484,
-5.12721978823511));
#21132=CARTESIAN_POINT('Ctrl Pts',(97.2966200000278,-0.949873001577503,
-5.12412980250489));
#21133=CARTESIAN_POINT('Ctrl Pts',(97.3323033642146,-0.915907160871423,
-5.12103981677467));
#21134=CARTESIAN_POINT('Ctrl Pts',(97.3679825338018,-0.881945312869059,
-5.11795019427402));
#21135=CARTESIAN_POINT('Ctrl Pts',(97.4016769579563,-0.845892907767278,
-5.11486057177336));
#21136=CARTESIAN_POINT('Ctrl Pts',(97.4331408293932,-0.808017950416858,
-5.11177094927271));
#21137=CARTESIAN_POINT('Ctrl Pts',(97.46463910441,-0.770101579404974,-5.1086779484823));
#21138=CARTESIAN_POINT('Ctrl Pts',(97.4939016034476,-0.730359108388724,
-5.10558494769189));
#21139=CARTESIAN_POINT('Ctrl Pts',(97.520723106248,-0.689091299624146,-5.10249194690149));
#21140=CARTESIAN_POINT('Ctrl Pts',(97.5475607781688,-0.647798612903396,
-5.09939708152121));
#21141=CARTESIAN_POINT('Ctrl Pts',(97.5719542521659,-0.604979243727851,
-5.09630221614094));
#21142=CARTESIAN_POINT('Ctrl Pts',(97.593743870321,-0.560959359015282,-5.09320735076066));
#21143=CARTESIAN_POINT('Ctrl Pts',(97.6155773230675,-0.516850918658907,
-5.09010625938052));
#21144=CARTESIAN_POINT('Ctrl Pts',(97.6347962528238,-0.471537656915443,
-5.08700516800038));
#21145=CARTESIAN_POINT('Ctrl Pts',(97.65128945544,-0.425364963724596,-5.08390407662024));
#21146=CARTESIAN_POINT('Ctrl Pts',(97.6598323048649,-0.401449271020396,
-5.0822978296511));
#21147=CARTESIAN_POINT('Ctrl Pts',(97.6676447099899,-0.377303239195462,
-5.08069158268195));
#21148=CARTESIAN_POINT('Ctrl Pts',(97.6747166060384,-0.35297594900736,-5.07908533571281));
#21149=CARTESIAN_POINT('Ctrl Pts',(97.6926205914113,-0.291386320893395,
-5.07501878523703));
#21150=CARTESIAN_POINT('Ctrl Pts',(97.705839977151,-0.22841490933399,-5.07095223476125));
#21151=CARTESIAN_POINT('Ctrl Pts',(97.7142116855971,-0.164679967083339,
-5.06688568428547));
#21152=CARTESIAN_POINT('Ctrl Pts',(97.7212827662567,-0.110846879083575,
-5.06345091268472));
#21153=CARTESIAN_POINT('Ctrl Pts',(97.7248961315897,-0.0564691825175074,
-5.06001614108397));
#21154=CARTESIAN_POINT('Ctrl Pts',(97.7249794730849,-0.00193236804568257,
-5.05658136948322));
#21155=CARTESIAN_POINT('',(97.4185971022994,0.825211298936501,-4.99999999999999));
#21156=CARTESIAN_POINT('Ctrl Pts',(97.7249794131076,-0.0019712252134486,
-5.05599185435273));
#21157=CARTESIAN_POINT('Ctrl Pts',(97.7250886418092,0.0680966313148683,
-5.05116780817991));
#21158=CARTESIAN_POINT('Ctrl Pts',(97.7193739476589,0.138060871914648,-5.04642730973536));
#21159=CARTESIAN_POINT('Ctrl Pts',(97.7015947191016,0.245097279283364,-5.03934388598835));
#21160=CARTESIAN_POINT('Ctrl Pts',(97.6935756686832,0.282690592057035,-5.03688714426543));
#21161=CARTESIAN_POINT('Ctrl Pts',(97.6733133589011,0.360187379727602,-5.0318677559316));
#21162=CARTESIAN_POINT('Ctrl Pts',(97.6607824801873,0.399967703886956,-5.0293170680671));
#21163=CARTESIAN_POINT('Ctrl Pts',(97.6293133272092,0.484960679704296,-5.02386746605508));
#21164=CARTESIAN_POINT('Ctrl Pts',(97.6096667059248,0.529838199790481,-5.02099038870329));
#21165=CARTESIAN_POINT('Ctrl Pts',(97.5529429615142,0.641312849549861,-5.01367877086113));
#21166=CARTESIAN_POINT('Ctrl Pts',(97.5123652844107,0.705898724599613,-5.00928432305277));
#21167=CARTESIAN_POINT('Ctrl Pts',(97.4509415607018,0.786501315358406,-5.00314001166332));
#21168=CARTESIAN_POINT('Ctrl Pts',(97.4350564634794,0.80610106640531,-5.00158722299082));
#21169=CARTESIAN_POINT('Ctrl Pts',(97.4185971022994,0.825211298936494,-4.99999999999999));
#21170=CARTESIAN_POINT('',(95.5154707437297,0.840188050881734,-4.99999999999999));
#21171=CARTESIAN_POINT('Origin',(96.460480949577,-1.44499066804254E-15,
-4.99999999999999));
#21172=CARTESIAN_POINT('Ctrl Pts',(95.5154707437297,0.840188050881728,-5.00000000000008));
#21173=CARTESIAN_POINT('Ctrl Pts',(95.5225653642979,0.848167798792328,-5.00069948174956));
#21174=CARTESIAN_POINT('Ctrl Pts',(95.5297607391518,0.856057327215644,-5.00140476782242));
#21175=CARTESIAN_POINT('Ctrl Pts',(95.6012645399553,0.932492002900971,-5.00836574119585));
#21176=CARTESIAN_POINT('Ctrl Pts',(95.6729242985494,0.993754826969376,-5.01494261410443));
#21177=CARTESIAN_POINT('Ctrl Pts',(95.8008995005763,1.08055089023169,-5.02546961385795));
#21178=CARTESIAN_POINT('Ctrl Pts',(95.8534778851055,1.11093969294436,-5.02951681756359));
#21179=CARTESIAN_POINT('Ctrl Pts',(95.9394869817854,1.15271315299406,-5.03568910567018));
#21180=CARTESIAN_POINT('Ctrl Pts',(95.9715545445553,1.16667634308418,-5.03790068992543));
#21181=CARTESIAN_POINT('Ctrl Pts',(96.041998665254,1.19393414997956,-5.04258437551926));
#21182=CARTESIAN_POINT('Ctrl Pts',(96.080520081999,1.20674621808099,-5.04503831417902));
#21183=CARTESIAN_POINT('Ctrl Pts',(96.213858882752,1.24407395621109,-5.05325544409173));
#21184=CARTESIAN_POINT('Ctrl Pts',(96.310864231887,1.25942725862804,-5.05874252092699));
#21185=CARTESIAN_POINT('Ctrl Pts',(96.440525397292,1.26474445598386,-5.06628278241473));
#21186=CARTESIAN_POINT('Ctrl Pts',(96.4724174834013,1.26484545460788,-5.0681567189018));
#21187=CARTESIAN_POINT('Ctrl Pts',(96.529406746253,1.26287043739154,-5.07159134821271));
#21188=CARTESIAN_POINT('Ctrl Pts',(96.5545027279978,1.26125025259789,-5.07313385778599));
#21189=CARTESIAN_POINT('Ctrl Pts',(96.6011390478585,1.25683992959629,-5.07608386292141));
#21190=CARTESIAN_POINT('Ctrl Pts',(96.6226871690055,1.25424088503172,-5.07748205493465));
#21191=CARTESIAN_POINT('Ctrl Pts',(96.7472870107203,1.23594820818855,-5.08573551993887));
#21192=CARTESIAN_POINT('Ctrl Pts',(96.8481467377453,1.20811437538997,-5.09304584406037));
#21193=CARTESIAN_POINT('Ctrl Pts',(96.9843978543938,1.15166901369871,-5.10307174950027));
#21194=CARTESIAN_POINT('Ctrl Pts',(97.0234783199235,1.13307766806414,-5.1059724254529));
#21195=CARTESIAN_POINT('Ctrl Pts',(97.095312182274,1.09426856446604,-5.11133259843523));
#21196=CARTESIAN_POINT('Ctrl Pts',(97.1282458624499,1.07448821477941,-5.11380250988762));
#21197=CARTESIAN_POINT('Ctrl Pts',(97.1898933542052,1.03353083741832,-5.11845965731787));
#21198=CARTESIAN_POINT('Ctrl Pts',(97.2187116403285,1.01257842015142,-5.12065238746011));
#21199=CARTESIAN_POINT('Ctrl Pts',(97.309501894184,0.940516391970181,-5.12765366954388));
#21200=CARTESIAN_POINT('Ctrl Pts',(97.3674990342575,0.884718984450137,-5.13226403185193));
#21201=CARTESIAN_POINT('Ctrl Pts',(97.4545673120993,0.783324805870413,-5.13991283324053));
#21202=CARTESIAN_POINT('Ctrl Pts',(97.4867201248125,0.74070102000269,-5.14295588062998));
#21203=CARTESIAN_POINT('Ctrl Pts',(97.5348262778599,0.667758395396185,-5.14809815860554));
#21204=CARTESIAN_POINT('Ctrl Pts',(97.5524116952355,0.638596875353117,-5.15013905273329));
#21205=CARTESIAN_POINT('Ctrl Pts',(97.5784666262472,0.591161262615176,-5.15349297607473));
#21206=CARTESIAN_POINT('Ctrl Pts',(97.5877128783719,0.573333833101893,-5.15476225805567));
#21207=CARTESIAN_POINT('Ctrl Pts',(97.6100278594998,0.527680517658497,-5.15803964687414));
#21208=CARTESIAN_POINT('Ctrl Pts',(97.6225120280938,0.49958808510192,-5.16007661248045));
#21209=CARTESIAN_POINT('Ctrl Pts',(97.6659179821178,0.391460251440093,-5.16792017719288));
#21210=CARTESIAN_POINT('Ctrl Pts',(97.6896921504058,0.308804017477303,-5.17390485661856));
#21211=CARTESIAN_POINT('Ctrl Pts',(97.7123961087576,0.182883262210213,-5.18259731786388));
#21212=CARTESIAN_POINT('Ctrl Pts',(97.7177980508486,0.141039475040924,-5.18542213923926));
#21213=CARTESIAN_POINT('Ctrl Pts',(97.7240536048506,0.0613846348084678,
-5.19066241450169));
#21214=CARTESIAN_POINT('Ctrl Pts',(97.7253228300527,0.0236525481661949,
-5.1930872464048));
#21215=CARTESIAN_POINT('Ctrl Pts',(97.724508896298,-0.049423421546514,-5.19768168968038));
#21216=CARTESIAN_POINT('Ctrl Pts',(97.722633830023,-0.0847337891276406,
-5.199855764321));
#21217=CARTESIAN_POINT('Ctrl Pts',(97.7116857605549,-0.19965364530648,-5.20682154140594));
#21218=CARTESIAN_POINT('Ctrl Pts',(97.6965321583009,-0.27848573892177,-5.21141410574877));
#21219=CARTESIAN_POINT('Ctrl Pts',(97.6590052371654,-0.406638089032292,
-5.2190452990109));
#21220=CARTESIAN_POINT('Ctrl Pts',(97.6407558255838,-0.456908756842203,
-5.22208874196325));
#21221=CARTESIAN_POINT('Ctrl Pts',(97.6057743355483,-0.537047928321703,
-5.22722850472882));
#21222=CARTESIAN_POINT('Ctrl Pts',(97.5909142954068,-0.567659607035057,
-5.22926569331807));
#21223=CARTESIAN_POINT('Ctrl Pts',(97.5653842407371,-0.615263561106463,
-5.23261055451799));
#21224=CARTESIAN_POINT('Ctrl Pts',(97.5555133475847,-0.632664578468388,
-5.23387410625749));
#21225=CARTESIAN_POINT('Ctrl Pts',(97.5296039548488,-0.675915083501862,
-5.23712341030891));
#21226=CARTESIAN_POINT('Ctrl Pts',(97.5130399457795,-0.701430270279938,
-5.23913720139458));
#21227=CARTESIAN_POINT('Ctrl Pts',(97.4463125762333,-0.796524620269645,
-5.24695058384691));
#21228=CARTESIAN_POINT('Ctrl Pts',(97.3900374604782,-0.861533870346743,
-5.25293176224602));
#21229=CARTESIAN_POINT('Ctrl Pts',(97.2966549355382,-0.949517074658011,
-5.2616499081229));
#21230=CARTESIAN_POINT('Ctrl Pts',(97.2642409619749,-0.97710799575487,-5.264500792442));
#21231=CARTESIAN_POINT('Ctrl Pts',(97.2003540777347,-1.0261539395934,-5.26978474217415));
#21232=CARTESIAN_POINT('Ctrl Pts',(97.1691831023805,-1.04792457598888,-5.27222743626958));
#21233=CARTESIAN_POINT('Ctrl Pts',(97.1070407871836,-1.08728313143618,-5.276853122785));
#21234=CARTESIAN_POINT('Ctrl Pts',(97.0762148323405,-1.10503230963672,-5.27904070096637));
#21235=CARTESIAN_POINT('Ctrl Pts',(96.9894653531937,-1.1502224079078,-5.28494476461941));
#21236=CARTESIAN_POINT('Ctrl Pts',(96.9322000730558,-1.17486949744465,-5.28856368211066));
#21237=CARTESIAN_POINT('Ctrl Pts',(96.8118973729564,-1.21642647252748,-5.29587426582507));
#21238=CARTESIAN_POINT('Ctrl Pts',(96.74890536976,-1.23288178663247,-5.29955174558859));
#21239=CARTESIAN_POINT('Ctrl Pts',(96.6479723017219,-1.25108656976633,-5.30555088141909));
#21240=CARTESIAN_POINT('Ctrl Pts',(96.6107387393857,-1.25610216849582,-5.30778747009319));
#21241=CARTESIAN_POINT('Ctrl Pts',(96.5533600376612,-1.26124390004,-5.31134397830249));
#21242=CARTESIAN_POINT('Ctrl Pts',(96.5333431143548,-1.26255840877144,-5.31260619177808));
#21243=CARTESIAN_POINT('Ctrl Pts',(96.4848206225441,-1.26458704372851,-5.31572651623737));
#21244=CARTESIAN_POINT('Ctrl Pts',(96.4563103700845,-1.26481426615795,-5.31760638510492));
#21245=CARTESIAN_POINT('Ctrl Pts',(96.338870680238,-1.26177984091943,-5.32547815892105));
#21246=CARTESIAN_POINT('Ctrl Pts',(96.2504141362109,-1.25009988050842,-5.33168995699856));
#21247=CARTESIAN_POINT('Ctrl Pts',(96.122477221436,-1.21923369593521,-5.34063361393174));
#21248=CARTESIAN_POINT('Ctrl Pts',(96.0815680163989,-1.20714659420612,-5.34349100484987));
#21249=CARTESIAN_POINT('Ctrl Pts',(96.0340575203261,-1.19045493739913,-5.34679512413616));
#21250=CARTESIAN_POINT('Ctrl Pts',(96.0267949549122,-1.18782841401933,-5.34729983970381));
#21251=CARTESIAN_POINT('Ctrl Pts',(96.0195573809006,-1.1851357123071,-5.34780246104807));
#21252=CARTESIAN_POINT('Origin',(96.460480949577,-1.62868768791465E-15,
-6.49999999999999));
#21253=CARTESIAN_POINT('',(96.0195573766758,-1.18513571073528,-5.84684438197146));
#21254=CARTESIAN_POINT('',(96.0195573765031,-1.18513571067102,-5.70991346827675));
#21255=CARTESIAN_POINT('',(96.0195573765031,-1.18513571067102,-6.49999999999999));
#21256=CARTESIAN_POINT('',(97.7249809164252,0.000289553175782366,-5.55658032643166));
#21257=CARTESIAN_POINT('Ctrl Pts',(96.019557376503,-1.18513571067102,-5.70991346827675));
#21258=CARTESIAN_POINT('Ctrl Pts',(96.0672300587458,-1.20287208398524,-5.70669551900282));
#21259=CARTESIAN_POINT('Ctrl Pts',(96.1160769577919,-1.21776546375623,-5.7034775697289));
#21260=CARTESIAN_POINT('Ctrl Pts',(96.1657252529368,-1.22966634877033,-5.70025962045498));
#21261=CARTESIAN_POINT('Ctrl Pts',(96.2137887264982,-1.24118734602841,-5.69714439123315));
#21262=CARTESIAN_POINT('Ctrl Pts',(96.2626026199803,-1.24990389543441,-5.69402916201133));
#21263=CARTESIAN_POINT('Ctrl Pts',(96.3118102439555,-1.25572977638105,-5.6909139327895));
#21264=CARTESIAN_POINT('Ctrl Pts',(96.3609731670002,-1.26155036501162,-5.68780153348779));
#21265=CARTESIAN_POINT('Ctrl Pts',(96.4105285703443,-1.26448542032649,-5.68468913418607));
#21266=CARTESIAN_POINT('Ctrl Pts',(96.4601105045368,-1.26449994573763,-5.68157673488436));
#21267=CARTESIAN_POINT('Ctrl Pts',(96.5096684816013,-1.26451446413035,-5.67846583943983));
#21268=CARTESIAN_POINT('Ctrl Pts',(96.5592524169426,-1.26161124898055,-5.67535494399531));
#21269=CARTESIAN_POINT('Ctrl Pts',(96.6084947901584,-1.25580737097548,-5.67224404855078));
#21270=CARTESIAN_POINT('Ctrl Pts',(96.6577343084241,-1.25000382946479,-5.66913333346822));
#21271=CARTESIAN_POINT('Ctrl Pts',(96.7066317603219,-1.24130002598907,-5.66602261838567));
#21272=CARTESIAN_POINT('Ctrl Pts',(96.7548257830587,-1.22976476165267,-5.66291190330311));
#21273=CARTESIAN_POINT('Ctrl Pts',(96.8030700054266,-1.2182174820085,-5.65979794805214));
#21274=CARTESIAN_POINT('Ctrl Pts',(96.8506088036549,-1.20383298721585,-5.65668399280118));
#21275=CARTESIAN_POINT('Ctrl Pts',(96.897093860719,-1.18673055738196,-5.65357003755021));
#21276=CARTESIAN_POINT('Ctrl Pts',(96.9436083605024,-1.16961729520598,-5.65045410998134));
#21277=CARTESIAN_POINT('Ctrl Pts',(96.9890672892405,-1.1497828924537,-5.64733818241247));
#21278=CARTESIAN_POINT('Ctrl Pts',(97.0331435518692,-1.12739424955777,-5.6442222548436));
#21279=CARTESIAN_POINT('Ctrl Pts',(97.0772978810094,-1.10496595259083,-5.64110080844031));
#21280=CARTESIAN_POINT('Ctrl Pts',(97.1200641889183,-1.07997467101853,-5.63797936203702));
#21281=CARTESIAN_POINT('Ctrl Pts',(97.1611427340333,-1.05263161352988,-5.63485791563373));
#21282=CARTESIAN_POINT('Ctrl Pts',(97.1706848147781,-1.04628013098259,-5.63413283899001));
#21283=CARTESIAN_POINT('Ctrl Pts',(97.1801359668656,-1.03980192374125,-5.6334077623463));
#21284=CARTESIAN_POINT('Ctrl Pts',(97.1894926961252,-1.03319994357083,-5.63268268570258));
#21285=CARTESIAN_POINT('Ctrl Pts',(97.2304118859496,-1.00432792298384,-5.62951175406629));
#21286=CARTESIAN_POINT('Ctrl Pts',(97.2697102211182,-0.972952719807752,
-5.62634082243));
#21287=CARTESIAN_POINT('Ctrl Pts',(97.3070638328496,-0.939285724234015,
-5.62316989079372));
#21288=CARTESIAN_POINT('Ctrl Pts',(97.3435475108083,-0.906402804285653,
-5.62007280745198));
#21289=CARTESIAN_POINT('Ctrl Pts',(97.3781756233914,-0.871334071940765,
-5.61697572411024));
#21290=CARTESIAN_POINT('Ctrl Pts',(97.4106760157132,-0.834319834530179,
-5.6138786407685));
#21291=CARTESIAN_POINT('Ctrl Pts',(97.4431443732015,-0.797342081138584,
-5.61078461014527));
#21292=CARTESIAN_POINT('Ctrl Pts',(97.4734887958835,-0.758423032899424,
-5.60769057952203));
#21293=CARTESIAN_POINT('Ctrl Pts',(97.5014737604642,-0.717839966622951,
-5.6045965488988));
#21294=CARTESIAN_POINT('Ctrl Pts',(97.5294434203483,-0.677279094818499,
-5.60150421036989));
#21295=CARTESIAN_POINT('Ctrl Pts',(97.5550558631182,-0.635056463904144,
-5.59841187184098));
#21296=CARTESIAN_POINT('Ctrl Pts',(97.5781173633259,-0.591480427962307,
-5.59531953331207));
#21297=CARTESIAN_POINT('Ctrl Pts',(97.6021925688477,-0.545988937310035,
-5.59209126607204));
#21298=CARTESIAN_POINT('Ctrl Pts',(97.6234869621405,-0.499022814786495,
-5.588862998832));
#21299=CARTESIAN_POINT('Ctrl Pts',(97.6418336145739,-0.450961340809636,
-5.58563473159197));
#21300=CARTESIAN_POINT('Ctrl Pts',(97.6594234474501,-0.404882455404688,
-5.58253963392015));
#21301=CARTESIAN_POINT('Ctrl Pts',(97.6743038976555,-0.357797411132342,
-5.57944453624833));
#21302=CARTESIAN_POINT('Ctrl Pts',(97.6863783994627,-0.310057562984182,
-5.5763494385765));
#21303=CARTESIAN_POINT('Ctrl Pts',(97.6984605247094,-0.262287573481037,
-5.57325238676278));
#21304=CARTESIAN_POINT('Ctrl Pts',(97.7077330754251,-0.213862503409765,
-5.57015533494906));
#21305=CARTESIAN_POINT('Ctrl Pts',(97.7141507901325,-0.165142910479476,
-5.56705828313533));
#21306=CARTESIAN_POINT('Ctrl Pts',(97.7205794615709,-0.116340140358935,
-5.56395594383761));
#21307=CARTESIAN_POINT('Ctrl Pts',(97.7241435458509,-0.0672423976822919,
-5.5608536045399));
#21308=CARTESIAN_POINT('Ctrl Pts',(97.7248497887175,-0.018212320294003,
-5.55775126524218));
#21309=CARTESIAN_POINT('Ctrl Pts',(97.7249386428695,-0.0120437256748006,
-5.55736095230534));
#21310=CARTESIAN_POINT('Ctrl Pts',(97.7249823282973,-0.0058761959988108,
-5.5569706393685));
#21311=CARTESIAN_POINT('Ctrl Pts',(97.7249809164252,0.000289553175783053,
-5.55658032643166));
#21312=CARTESIAN_POINT('Ctrl Pts',(97.724980916425,0.00028955398282956,
-5.55658032638057));
#21313=CARTESIAN_POINT('Ctrl Pts',(97.7249773196589,0.0159968514554625,
-5.55558600091696));
#21314=CARTESIAN_POINT('Ctrl Pts',(97.7246810658307,0.0317004476496653,
-5.55459167545336));
#21315=CARTESIAN_POINT('Ctrl Pts',(97.7240925016085,0.0473929907538893,
-5.55359734998976));
#21316=CARTESIAN_POINT('Ctrl Pts',(97.7222443974738,0.0966679087703951,
-5.55047514695516));
#21317=CARTESIAN_POINT('Ctrl Pts',(97.7175057083344,0.145942192786499,-5.54735294392056));
#21318=CARTESIAN_POINT('Ctrl Pts',(97.7098783470884,0.194849667928159,-5.54423074088596));
#21319=CARTESIAN_POINT('Ctrl Pts',(97.7022649183057,0.243667806590612,-5.54111424100053));
#21320=CARTESIAN_POINT('Ctrl Pts',(97.6917733667566,0.292119928404832,-5.53799774111509));
#21321=CARTESIAN_POINT('Ctrl Pts',(97.6784574996112,0.339843160247207,-5.53488124122966));
#21322=CARTESIAN_POINT('Ctrl Pts',(97.6651550390072,0.387518343886712,-5.5317678790659));
#21323=CARTESIAN_POINT('Ctrl Pts',(97.6490340389043,0.434465565284101,-5.52865451690213));
#21324=CARTESIAN_POINT('Ctrl Pts',(97.6301992689561,0.480332492455985,-5.52554115473836));
#21325=CARTESIAN_POINT('Ctrl Pts',(97.6113754586339,0.526172730458223,-5.52242960418605));
#21326=CARTESIAN_POINT('Ctrl Pts',(97.5898412146458,0.570933413838964,-5.51931805363375));
#21327=CARTESIAN_POINT('Ctrl Pts',(97.5657501871831,0.614280198607817,-5.51620650308144));
#21328=CARTESIAN_POINT('Ctrl Pts',(97.5416629416409,0.657620178598667,-5.51309544099467));
#21329=CARTESIAN_POINT('Ctrl Pts',(97.5150199764645,0.699546222686597,-5.50998437890791));
#21330=CARTESIAN_POINT('Ctrl Pts',(97.4860206310223,0.739749019452612,-5.50687331682114));
#21331=CARTESIAN_POINT('Ctrl Pts',(97.4569931298087,0.779990849539505,-5.50375923417126));
#21332=CARTESIAN_POINT('Ctrl Pts',(97.4256050027741,0.818505647624967,-5.50064515152139));
#21333=CARTESIAN_POINT('Ctrl Pts',(97.3920975747538,0.855015037115848,-5.49753106887151));
#21334=CARTESIAN_POINT('Ctrl Pts',(97.3585719136484,0.891544293210746,-5.49441529169188));
#21335=CARTESIAN_POINT('Ctrl Pts',(97.322925049016,0.92606558632132,-5.49129951451225));
#21336=CARTESIAN_POINT('Ctrl Pts',(97.2854345824381,0.95833801637487,-5.48818373733262));
#21337=CARTESIAN_POINT('Ctrl Pts',(97.2478753372162,0.990669652252652,-5.48506224406171));
#21338=CARTESIAN_POINT('Ctrl Pts',(97.2084661758971,1.02074385925813,-5.4819407507908));
#21339=CARTESIAN_POINT('Ctrl Pts',(97.1675157658607,1.04836158769895,-5.47881925751989));
#21340=CARTESIAN_POINT('Ctrl Pts',(97.1486804028236,1.06106451157642,-5.47738350977222));
#21341=CARTESIAN_POINT('Ctrl Pts',(97.129519342501,1.07324837335567,-5.47594776202456));
#21342=CARTESIAN_POINT('Ctrl Pts',(97.1100642892041,1.08489710796872,-5.4745120142769));
#21343=CARTESIAN_POINT('Ctrl Pts',(97.0677616465199,1.11022586191971,-5.47139015575371));
#21344=CARTESIAN_POINT('Ctrl Pts',(97.0238829786064,1.13313200228666,-5.46826829723051));
#21345=CARTESIAN_POINT('Ctrl Pts',(96.9787361896904,1.15341742491392,-5.46514643870732));
#21346=CARTESIAN_POINT('Ctrl Pts',(96.933671681372,1.17366587710011,-5.46203026981104));
#21347=CARTESIAN_POINT('Ctrl Pts',(96.8873441317738,1.19130286203269,-5.45891410091476));
#21348=CARTESIAN_POINT('Ctrl Pts',(96.8400869848865,1.20617557095001,-5.45579793201849));
#21349=CARTESIAN_POINT('Ctrl Pts',(96.7928772909562,1.22103334553333,-5.45268489220295));
#21350=CARTESIAN_POINT('Ctrl Pts',(96.7447403678977,1.23313217566415,-5.44957185238742));
#21351=CARTESIAN_POINT('Ctrl Pts',(96.6960286204964,1.24236771719344,-5.44645881257189));
#21352=CARTESIAN_POINT('Ctrl Pts',(96.6473450773759,1.25159791131024,-5.44334757521785));
#21353=CARTESIAN_POINT('Ctrl Pts',(96.5980879066095,1.25796799945789,-5.44023633786381));
#21354=CARTESIAN_POINT('Ctrl Pts',(96.5486210950282,1.26142441896446,-5.43712510050977));
#21355=CARTESIAN_POINT('Ctrl Pts',(96.4991618960032,1.26488030655505,-5.43401434195088));
#21356=CARTESIAN_POINT('Ctrl Pts',(96.4494936665463,1.26542337874327,-5.43090358339198));
#21357=CARTESIAN_POINT('Ctrl Pts',(96.3999843288109,1.26305202144483,-5.42779282483309));
#21358=CARTESIAN_POINT('Ctrl Pts',(96.3504266505215,1.26067834877054,-5.42467902895238));
#21359=CARTESIAN_POINT('Ctrl Pts',(96.3010287218844,1.2553845929793,-5.42156523307166));
#21360=CARTESIAN_POINT('Ctrl Pts',(96.2521554339637,1.24722120313296,-5.41845143719094));
#21361=CARTESIAN_POINT('Ctrl Pts',(96.2032554051967,1.23905334671679,-5.41533593760784));
#21362=CARTESIAN_POINT('Ctrl Pts',(96.154881123348,1.22801285186346,-5.41222043802474));
#21363=CARTESIAN_POINT('Ctrl Pts',(96.1073858474992,1.21420101255461,-5.40910493844164));
#21364=CARTESIAN_POINT('Ctrl Pts',(96.0598031697776,1.20036375638901,-5.40598370564627));
#21365=CARTESIAN_POINT('Ctrl Pts',(96.0131032424064,1.1837451619834,-5.4028624728509));
#21366=CARTESIAN_POINT('Ctrl Pts',(95.9676211855102,1.16449538554863,-5.39974124005553));
#21367=CARTESIAN_POINT('Ctrl Pts',(95.9466641743868,1.15562556288895,-5.39830305289172));
#21368=CARTESIAN_POINT('Ctrl Pts',(95.9259654073852,1.14619775605937,-5.39686486572792));
#21369=CARTESIAN_POINT('Ctrl Pts',(95.9055557978332,1.13622987373246,-5.39542667856412));
#21370=CARTESIAN_POINT('Ctrl Pts',(95.8612893983061,1.11461053503822,-5.3923073946099));
#21371=CARTESIAN_POINT('Ctrl Pts',(95.818190521751,1.09035270442906,-5.38918811065567));
#21372=CARTESIAN_POINT('Ctrl Pts',(95.7765928412365,1.06360580351487,-5.38606882670145));
#21373=CARTESIAN_POINT('Ctrl Pts',(95.7350712395224,1.03690782052367,-5.38295524766581));
#21374=CARTESIAN_POINT('Ctrl Pts',(95.6950458466465,1.00773009012625,-5.37984166863018));
#21375=CARTESIAN_POINT('Ctrl Pts',(95.656826359082,0.976268174825118,-5.37672808959454));
#21376=CARTESIAN_POINT('Ctrl Pts',(95.6186453699179,0.944837951037592,-5.37361764685978));
#21377=CARTESIAN_POINT('Ctrl Pts',(95.5822671067884,0.911128444320484,-5.37050720412501));
#21378=CARTESIAN_POINT('Ctrl Pts',(95.5479710293874,0.87537757313946,-5.36739676139025));
#21379=CARTESIAN_POINT('Ctrl Pts',(95.5136948509245,0.83964744498297,-5.36428812336647));
#21380=CARTESIAN_POINT('Ctrl Pts',(95.4814988442001,0.80187869411898,-5.36117948534269));
#21381=CARTESIAN_POINT('Ctrl Pts',(95.4516262505552,0.762346670656862,-5.35807084731891));
#21382=CARTESIAN_POINT('Ctrl Pts',(95.4217582318716,0.722820701489285,-5.3549626853803));
#21383=CARTESIAN_POINT('Ctrl Pts',(95.3942132496516,0.681532434250401,-5.35185452344169));
#21384=CARTESIAN_POINT('Ctrl Pts',(95.3691931651421,0.638788870866742,-5.34874636150309));
#21385=CARTESIAN_POINT('Ctrl Pts',(95.3441484327452,0.596003199769932,-5.34563513763934));
#21386=CARTESIAN_POINT('Ctrl Pts',(95.3216338405391,0.551759845614649,-5.34252391377559));
#21387=CARTESIAN_POINT('Ctrl Pts',(95.3018059666686,0.506391680403736,-5.33941268991184));
#21388=CARTESIAN_POINT('Ctrl Pts',(95.2819671688355,0.460998520070124,-5.33629975195139));
#21389=CARTESIAN_POINT('Ctrl Pts',(95.2648182263788,0.414479830365957,-5.33318681399095));
#21390=CARTESIAN_POINT('Ctrl Pts',(95.250466754593,0.367186462083226,-5.3300738760305));
#21391=CARTESIAN_POINT('Ctrl Pts',(95.2360886407396,0.319805298406776,-5.32695515921302));
#21392=CARTESIAN_POINT('Ctrl Pts',(95.2245184892159,0.271647120120269,-5.32383644239554));
#21393=CARTESIAN_POINT('Ctrl Pts',(95.2158130647497,0.223074217424636,-5.32071772557806));
#21394=CARTESIAN_POINT('Ctrl Pts',(95.2117410621182,0.200354017121378,-5.3192589313358));
#21395=CARTESIAN_POINT('Ctrl Pts',(95.2082951045729,0.177543161626589,-5.31780013709354));
#21396=CARTESIAN_POINT('Ctrl Pts',(95.2054770925123,0.154678921487683,-5.31634134285128));
#21397=CARTESIAN_POINT('Ctrl Pts',(95.1994370883039,0.105672705868238,-5.31321462686395));
#21398=CARTESIAN_POINT('Ctrl Pts',(95.1962587973972,0.0562066151787424,
-5.31008791087661));
#21399=CARTESIAN_POINT('Ctrl Pts',(95.1959984009778,0.00664336421897154,
-5.30696119488927));
#21400=CARTESIAN_POINT('Ctrl Pts',(95.1957384816704,-0.0428290743508711,
-5.30384020783509));
#21401=CARTESIAN_POINT('Ctrl Pts',(95.1983858545174,-0.0923977783162371,
-5.3007192207809));
#21402=CARTESIAN_POINT('Ctrl Pts',(95.2039449368609,-0.141695090766752,
-5.29759823372672));
#21403=CARTESIAN_POINT('Ctrl Pts',(95.2094983944853,-0.190942523845796,
-5.29448040450944));
#21404=CARTESIAN_POINT('Ctrl Pts',(95.2179576673769,-0.239918569063965,
-5.29136257529216));
#21405=CARTESIAN_POINT('Ctrl Pts',(95.2292751844159,-0.288257894660407,
-5.28824474607488));
#21406=CARTESIAN_POINT('Ctrl Pts',(95.2405860216583,-0.336568689541037,
-5.28512875705496));
#21407=CARTESIAN_POINT('Ctrl Pts',(95.2547516361753,-0.384242978755336,
-5.28201276803504));
#21408=CARTESIAN_POINT('Ctrl Pts',(95.2716733384852,-0.430925415600221,
-5.27889677901512));
#21409=CARTESIAN_POINT('Ctrl Pts',(95.288592186744,-0.477599978883804,-5.27578131554469));
#21410=CARTESIAN_POINT('Ctrl Pts',(95.3082660128915,-0.52328250925045,-5.27266585207425));
#21411=CARTESIAN_POINT('Ctrl Pts',(95.3305470313202,-0.567635085572367,
-5.26955038860382));
#21412=CARTESIAN_POINT('Ctrl Pts',(95.3528490062695,-0.612029377926409,
-5.26643199486901));
#21413=CARTESIAN_POINT('Ctrl Pts',(95.3777628229908,-0.655090730421877,
-5.2633136011342));
#21414=CARTESIAN_POINT('Ctrl Pts',(95.4050943116575,-0.696505057053423,
-5.2601952073994));
#21415=CARTESIAN_POINT('Ctrl Pts',(95.4324402504819,-0.737941279438834,
-5.25707516496987));
#21416=CARTESIAN_POINT('Ctrl Pts',(95.4622060799938,-0.777728303751934,
-5.25395512254034));
#21417=CARTESIAN_POINT('Ctrl Pts',(95.4941558127478,-0.81558321459684,-5.25083508011081));
#21418=CARTESIAN_POINT('Ctrl Pts',(95.5261628610009,-0.853506034401186,
-5.24770944055188));
#21419=CARTESIAN_POINT('Ctrl Pts',(95.5603612553392,-0.889489427160365,
-5.24458380099294));
#21420=CARTESIAN_POINT('Ctrl Pts',(95.5964776307581,-0.923286800008501,
-5.241458161434));
#21421=CARTESIAN_POINT('Ctrl Pts',(95.6126627537539,-0.938432689653773,
-5.24005744333549));
#21422=CARTESIAN_POINT('Ctrl Pts',(95.6292326148829,-0.953140105703813,
-5.23865672523698));
#21423=CARTESIAN_POINT('Ctrl Pts',(95.6461606096548,-0.967389597829645,
-5.23725600713846));
#21424=CARTESIAN_POINT('Ctrl Pts',(95.6838682375086,-0.999130778839254,
-5.23413586458772));
#21425=CARTESIAN_POINT('Ctrl Pts',(95.7235161537926,-1.02873270917244,-5.23101572203697));
#21426=CARTESIAN_POINT('Ctrl Pts',(95.764832046977,-1.05595116094986,-5.22789557948622));
#21427=CARTESIAN_POINT('Ctrl Pts',(95.8060827129411,-1.0831266417587,-5.22478036284194));
#21428=CARTESIAN_POINT('Ctrl Pts',(95.8489956849724,-1.10792579976192,-5.22166514619765));
#21429=CARTESIAN_POINT('Ctrl Pts',(95.8932660745554,-1.13014491794379,-5.21854992955337));
#21430=CARTESIAN_POINT('Ctrl Pts',(95.9342862709442,-1.15073277813646,-5.21566342234739));
#21431=CARTESIAN_POINT('Ctrl Pts',(95.9764712566442,-1.16910574402079,-5.21277691514142));
#21432=CARTESIAN_POINT('Ctrl Pts',(96.019557376503,-1.18513571067102,-5.20989040793544));
#21433=CARTESIAN_POINT('Ctrl Pts',(96.0195573809006,-1.1851357123071,-5.34780246104807));
#21434=CARTESIAN_POINT('Ctrl Pts',(95.9911569000717,-1.17456946134598,-5.34977476389832));
#21435=CARTESIAN_POINT('Ctrl Pts',(95.9631412136764,-1.16298419416518,-5.35171447379949));
#21436=CARTESIAN_POINT('Ctrl Pts',(95.90327232285,-1.13566663154017,-5.35585319061882));
#21437=CARTESIAN_POINT('Ctrl Pts',(95.8716126124167,-1.11957787589962,-5.35803753528189));
#21438=CARTESIAN_POINT('Ctrl Pts',(95.7789345827735,-1.06746016986719,-5.3644562136911));
#21439=CARTESIAN_POINT('Ctrl Pts',(95.7202229885252,-1.02761682618313,-5.36854852764157));
#21440=CARTESIAN_POINT('Ctrl Pts',(95.6189843420318,-0.945711492749465,
-5.37600713338699));
#21441=CARTESIAN_POINT('Ctrl Pts',(95.5755077621782,-0.90515664375042,-5.37937733454893));
#21442=CARTESIAN_POINT('Ctrl Pts',(95.5105522626955,-0.83539656903172,-5.38496567420744));
#21443=CARTESIAN_POINT('Ctrl Pts',(95.4871955589494,-0.808063728116267,
-5.38711171708948));
#21444=CARTESIAN_POINT('Ctrl Pts',(95.4526231581329,-0.763929410360917,
-5.39057770429406));
#21445=CARTESIAN_POINT('Ctrl Pts',(95.4405921891734,-0.747791615837261,
-5.39184654568825));
#21446=CARTESIAN_POINT('Ctrl Pts',(95.4119352009272,-0.707373664449688,
-5.39503503107707));
#21447=CARTESIAN_POINT('Ctrl Pts',(95.3957641140544,-0.68279091753971,-5.39697912929723));
#21448=CARTESIAN_POINT('Ctrl Pts',(95.3360646053247,-0.584753256546981,
-5.40468531555168));
#21449=CARTESIAN_POINT('Ctrl Pts',(95.2991616379038,-0.507529482456535,
-5.41063881200647));
#21450=CARTESIAN_POINT('Ctrl Pts',(95.25568171314,-0.386389557460924,-5.41939549697864));
#21451=CARTESIAN_POINT('Ctrl Pts',(95.2431477106545,-0.344874589527996,
-5.4223044136229));
#21452=CARTESIAN_POINT('Ctrl Pts',(95.2235853959167,-0.265557153639341,
-5.42767121299091));
#21453=CARTESIAN_POINT('Ctrl Pts',(95.2160996080811,-0.227918425065709,
-5.43013994231391));
#21454=CARTESIAN_POINT('Ctrl Pts',(95.2050354991081,-0.155117492968852,
-5.43477567850614));
#21455=CARTESIAN_POINT('Ctrl Pts',(95.2011964767379,-0.120032138127394,
-5.4369490404489));
#21456=CARTESIAN_POINT('Ctrl Pts',(95.1945281719033,-0.0208555097307459,
-5.44295631467797));
#21457=CARTESIAN_POINT('Ctrl Pts',(95.1950984234687,0.0433559873195874,
-5.44668207222266));
#21458=CARTESIAN_POINT('Ctrl Pts',(95.2060335266596,0.171814811897757,-5.45408280060719));
#21459=CARTESIAN_POINT('Ctrl Pts',(95.2164833048842,0.235855473965022,-5.45774685108397));
#21460=CARTESIAN_POINT('Ctrl Pts',(95.2382788696431,0.325477382579932,-5.46314058223971));
#21461=CARTESIAN_POINT('Ctrl Pts',(95.2456302431665,0.351924731694582,-5.46476713914104));
#21462=CARTESIAN_POINT('Ctrl Pts',(95.2606510269022,0.399859856810959,-5.46781380157456));
#21463=CARTESIAN_POINT('Ctrl Pts',(95.2680526852936,0.421419520839781,-5.46922165092735));
#21464=CARTESIAN_POINT('Ctrl Pts',(95.2839999685176,0.46408033147565,-5.47210512927408));
#21465=CARTESIAN_POINT('Ctrl Pts',(95.2925410006007,0.485174355205833,-5.47358010934124));
#21466=CARTESIAN_POINT('Ctrl Pts',(95.3275518094054,0.565351795659446,-5.47934656150149));
#21467=CARTESIAN_POINT('Ctrl Pts',(95.3579736012902,0.622597227349399,-5.48379989415675));
#21468=CARTESIAN_POINT('Ctrl Pts',(95.4369365650063,0.747099177359437,-5.49393907156166));
#21469=CARTESIAN_POINT('Ctrl Pts',(95.4879838728063,0.812436735179592,-5.49959040755326));
#21470=CARTESIAN_POINT('Ctrl Pts',(95.5707645980753,0.899307558863883,-5.50744234627463));
#21471=CARTESIAN_POINT('Ctrl Pts',(95.5976575433849,0.925140810355008,-5.50983214883126));
#21472=CARTESIAN_POINT('Ctrl Pts',(95.6526545435528,0.97348289400719,-5.51442692831463));
#21473=CARTESIAN_POINT('Ctrl Pts',(95.6806554955213,0.996054770724119,-5.51663337792311));
#21474=CARTESIAN_POINT('Ctrl Pts',(95.7933515840982,1.07923043364241,-5.52506688512126));
#21475=CARTESIAN_POINT('Ctrl Pts',(95.884432419787,1.13047301025196,-5.53091475101771));
#21476=CARTESIAN_POINT('Ctrl Pts',(96.0305736855713,1.19039386961959,-5.54000351161491));
#21477=CARTESIAN_POINT('Ctrl Pts',(96.0816266759806,1.20761168217657,-5.54313883687816));
#21478=CARTESIAN_POINT('Ctrl Pts',(96.1540553835878,1.22699281191022,-5.54772527459907));
#21479=CARTESIAN_POINT('Ctrl Pts',(96.1746291829358,1.23194833939761,-5.54904367072386));
#21480=CARTESIAN_POINT('Ctrl Pts',(96.219963501988,1.24167103994746,-5.55199977182372));
#21481=CARTESIAN_POINT('Ctrl Pts',(96.2447599762878,1.24621822194121,-5.55364699100465));
#21482=CARTESIAN_POINT('Ctrl Pts',(96.3682399093674,1.26506661771489,-5.56194546564313));
#21483=CARTESIAN_POINT('Ctrl Pts',(96.4682380348751,1.26840149237045,-5.56893398562525));
#21484=CARTESIAN_POINT('Ctrl Pts',(96.6087947827134,1.2564526695749,-5.57850074490316));
#21485=CARTESIAN_POINT('Ctrl Pts',(96.6498052997827,1.25093051067384,-5.58126580767854));
#21486=CARTESIAN_POINT('Ctrl Pts',(96.7272659469987,1.2366025684872,-5.58642331452262));
#21487=CARTESIAN_POINT('Ctrl Pts',(96.763739664481,1.22816724521475,-5.58882377700623));
#21488=CARTESIAN_POINT('Ctrl Pts',(96.8343130364044,1.20850908797719,-5.59342303737393));
#21489=CARTESIAN_POINT('Ctrl Pts',(96.8684150080584,1.19742842961825,-5.59562401266924));
#21490=CARTESIAN_POINT('Ctrl Pts',(96.9550254467938,1.16515566383876,-5.60119219493759));
#21491=CARTESIAN_POINT('Ctrl Pts',(97.0066647780769,1.14186082303937,-5.60448845585805));
#21492=CARTESIAN_POINT('Ctrl Pts',(97.1166070746032,1.08309390435397,-5.61165866907361));
#21493=CARTESIAN_POINT('Ctrl Pts',(97.1739479409225,1.0462112655269,-5.61550121643613));
#21494=CARTESIAN_POINT('Ctrl Pts',(97.2585360174733,0.981601246340045,-5.62171816321294));
#21495=CARTESIAN_POINT('Ctrl Pts',(97.2879535081073,0.95693337407692,-5.62400001451163));
#21496=CARTESIAN_POINT('Ctrl Pts',(97.3311109753079,0.91726426748031,-5.62761572486773));
#21497=CARTESIAN_POINT('Ctrl Pts',(97.3456866604919,0.903206045813647,-5.62888890415512));
#21498=CARTESIAN_POINT('Ctrl Pts',(97.3797282065796,0.868757099131709,-5.63199914778414));
#21499=CARTESIAN_POINT('Ctrl Pts',(97.3988589496941,0.848057111250292,-5.63385644742696));
#21500=CARTESIAN_POINT('Ctrl Pts',(97.4932599148953,0.738805001983189,-5.64352554337023));
#21501=CARTESIAN_POINT('Ctrl Pts',(97.5567590509556,0.640815893675838,-5.65170272432219));
#21502=CARTESIAN_POINT('Ctrl Pts',(97.624608990299,0.495681461212182,-5.66237780665581));
#21503=CARTESIAN_POINT('Ctrl Pts',(97.6411439949906,0.454895306835878,-5.66524761896211));
#21504=CARTESIAN_POINT('Ctrl Pts',(97.666693488182,0.381024614454803,-5.67022208190327));
#21505=CARTESIAN_POINT('Ctrl Pts',(97.6765520425905,0.348281354497011,-5.67235299087159));
#21506=CARTESIAN_POINT('Ctrl Pts',(97.6974434641501,0.267109409052004,-5.67747840266826));
#21507=CARTESIAN_POINT('Ctrl Pts',(97.7069746336448,0.218352953423642,-5.68042208732178));
#21508=CARTESIAN_POINT('Ctrl Pts',(97.7247682415555,0.0865364592984473,
-5.68816673857076));
#21509=CARTESIAN_POINT('Ctrl Pts',(97.7277224927789,0.00301850559099509,
-5.69284191243654));
#21510=CARTESIAN_POINT('Ctrl Pts',(97.7197790382627,-0.122003240281741,
-5.70012514228139));
#21511=CARTESIAN_POINT('Ctrl Pts',(97.7150445459317,-0.163664092197564,
-5.70260338958254));
#21512=CARTESIAN_POINT('Ctrl Pts',(97.7049333509116,-0.225205217198401,
-5.70643980817995));
#21513=CARTESIAN_POINT('Ctrl Pts',(97.7011258855457,-0.245314622744633,
-5.70772265893581));
#21514=CARTESIAN_POINT('Ctrl Pts',(97.6910712438335,-0.29216676648176,-5.71079259891487));
#21515=CARTESIAN_POINT('Ctrl Pts',(97.6844388985957,-0.318811171856491,
-5.71259729145879));
#21516=CARTESIAN_POINT('Ctrl Pts',(97.6540060586253,-0.426049695415381,
-5.72004548788207));
#21517=CARTESIAN_POINT('Ctrl Pts',(97.6230676157072,-0.504393161237666,
-5.72590078850343));
#21518=CARTESIAN_POINT('Ctrl Pts',(97.5551479600919,-0.63623666745809,-5.73602116168861));
#21519=CARTESIAN_POINT('Ctrl Pts',(97.5213891236651,-0.691063609654764,
-5.74032580274532));
#21520=CARTESIAN_POINT('Ctrl Pts',(97.4630779210482,-0.771348987121128,
-5.74673990758684));
#21521=CARTESIAN_POINT('Ctrl Pts',(97.4413912258913,-0.798746123787804,
-5.7489525405346));
#21522=CARTESIAN_POINT('Ctrl Pts',(97.3929295453079,-0.855012681242475,
-5.7535629459878));
#21523=CARTESIAN_POINT('Ctrl Pts',(97.3658850299456,-0.883601158678016,
-5.75594614704933));
#21524=CARTESIAN_POINT('Ctrl Pts',(97.3048552130503,-0.942365258674599,
-5.76098159174631));
#21525=CARTESIAN_POINT('Ctrl Pts',(97.2704882598381,-0.972064181601018,
-5.76361472503132));
#21526=CARTESIAN_POINT('Ctrl Pts',(97.1680173257085,-1.05140028897219,-5.77106291245415));
#21527=CARTESIAN_POINT('Ctrl Pts',(97.0964618159717,-1.09616428050218,-5.77579065737659));
#21528=CARTESIAN_POINT('Ctrl Pts',(96.9964450239804,-1.14562340095486,-5.78244751105435));
#21529=CARTESIAN_POINT('Ctrl Pts',(96.9715069925848,-1.15696265706459,-5.78411223895859));
#21530=CARTESIAN_POINT('Ctrl Pts',(96.927585730249,-1.17523650367237,-5.78708560849603));
#21531=CARTESIAN_POINT('Ctrl Pts',(96.9087692567348,-1.1825417965678,-5.78837421224998));
#21532=CARTESIAN_POINT('Ctrl Pts',(96.8521939510208,-1.20296240868748,-5.79228437359231));
#21533=CARTESIAN_POINT('Ctrl Pts',(96.8139819051272,-1.21474033511454,-5.79496791798944));
#21534=CARTESIAN_POINT('Ctrl Pts',(96.7031121126548,-1.2432388238697,-5.8027595527477));
#21535=CARTESIAN_POINT('Ctrl Pts',(96.6294443888879,-1.25537434724787,-5.80793410682928));
#21536=CARTESIAN_POINT('Ctrl Pts',(96.4987825688458,-1.26518244348814,-5.81681911679945));
#21537=CARTESIAN_POINT('Ctrl Pts',(96.442205178669,-1.26563072099937,-5.82057393355728));
#21538=CARTESIAN_POINT('Ctrl Pts',(96.3513241613236,-1.26025253574166,-5.82643669795251));
#21539=CARTESIAN_POINT('Ctrl Pts',(96.3169631995085,-1.25680336256803,-5.82861523157875));
#21540=CARTESIAN_POINT('Ctrl Pts',(96.2422089631943,-1.24619302269063,-5.83328648687228));
#21541=CARTESIAN_POINT('Ctrl Pts',(96.2019356704957,-1.2384646074627,-5.83575855646203));
#21542=CARTESIAN_POINT('Ctrl Pts',(96.1145052424056,-1.21723474422539,-5.84108183283655));
#21543=CARTESIAN_POINT('Ctrl Pts',(96.0676147706023,-1.2029198833253,-5.84390774147123));
#21544=CARTESIAN_POINT('Ctrl Pts',(96.0209661975241,-1.18565914050278,-5.84675826449389));
#21545=CARTESIAN_POINT('Ctrl Pts',(96.0202616618289,-1.1853977363609,-5.84680132585598));
#21546=CARTESIAN_POINT('Ctrl Pts',(96.0195573766758,-1.18513571073528,-5.84684438197146));
#21547=CARTESIAN_POINT('Origin',(96.460480949577,-1.62868768791465E-15,
-6.49999999999999));
#21548=CARTESIAN_POINT('',(96.0195573796018,-1.18513571182388,-6.34560991122238));
#21549=CARTESIAN_POINT('',(96.0195573765031,-1.18513571067102,-6.20996462145127));
#21550=CARTESIAN_POINT('',(96.0195573765031,-1.18513571067102,-6.49999999999999));
#21551=CARTESIAN_POINT('',(95.5023647968546,0.825211298936472,-6.49999999999999));
#21552=CARTESIAN_POINT('Ctrl Pts',(96.0195573796018,-1.18513571182389,-6.34560991122238));
#21553=CARTESIAN_POINT('Ctrl Pts',(96.0042740283813,-1.17944962059055,-6.34669630916491));
#21554=CARTESIAN_POINT('Ctrl Pts',(95.9891013983046,-1.1734681624746,-6.34779485622615));
#21555=CARTESIAN_POINT('Ctrl Pts',(95.8749001292853,-1.12587434226586,-6.35619519895383));
#21556=CARTESIAN_POINT('Ctrl Pts',(95.7814167343244,-1.07208871018347,-6.36378134632822));
#21557=CARTESIAN_POINT('Ctrl Pts',(95.6595252904877,-0.979545956375136,
-6.37406645688343));
#21558=CARTESIAN_POINT('Ctrl Pts',(95.6247163845456,-0.950020376918963,
-6.37706580422017));
#21559=CARTESIAN_POINT('Ctrl Pts',(95.5676186247547,-0.896015886562431,
-6.38209833101502));
#21560=CARTESIAN_POINT('Ctrl Pts',(95.5445557459024,-0.872427050716327,
-6.38416743703659));
#21561=CARTESIAN_POINT('Ctrl Pts',(95.4935501700806,-0.816003097838945,
-6.3888484446704));
#21562=CARTESIAN_POINT('Ctrl Pts',(95.466310880474,-0.782587158110073,-6.39142875336817));
#21563=CARTESIAN_POINT('Ctrl Pts',(95.3729586430953,-0.655305243335814,
-6.40070552326952));
#21564=CARTESIAN_POINT('Ctrl Pts',(95.3180106426798,-0.553973072196473,
-6.40701751053078));
#21565=CARTESIAN_POINT('Ctrl Pts',(95.2678495498594,-0.421111348337773,
-6.41549320788654));
#21566=CARTESIAN_POINT('Ctrl Pts',(95.2590433970342,-0.395287199291953,
-6.41715199240577));
#21567=CARTESIAN_POINT('Ctrl Pts',(95.2451667610324,-0.349831138929065,
-6.42012514201814));
#21568=CARTESIAN_POINT('Ctrl Pts',(95.2397209063265,-0.330325748199002,
-6.42141960070249));
#21569=CARTESIAN_POINT('Ctrl Pts',(95.225408013026,-0.273860241682951,-6.42521202014989));
#21570=CARTESIAN_POINT('Ctrl Pts',(95.2177364137455,-0.236622123974852,
-6.42776497095821));
#21571=CARTESIAN_POINT('Ctrl Pts',(95.2016561848986,-0.135768792923902,
-6.4347300985314));
#21572=CARTESIAN_POINT('Ctrl Pts',(95.1963912129465,-0.0717630770358149,
-6.43919968672181));
#21573=CARTESIAN_POINT('Ctrl Pts',(95.1955571551129,0.0663688831531573,
-6.44871677454101));
#21574=CARTESIAN_POINT('Ctrl Pts',(95.2016076488731,0.140278435494044,-6.45372531453812));
#21575=CARTESIAN_POINT('Ctrl Pts',(95.2205944501537,0.251254509108818,-6.46106008424667));
#21576=CARTESIAN_POINT('Ctrl Pts',(95.2288335269183,0.288950656981483,-6.46352043213571));
#21577=CARTESIAN_POINT('Ctrl Pts',(95.2500298226118,0.368332320856639,-6.46865690033929));
#21578=CARTESIAN_POINT('Ctrl Pts',(95.263447158062,0.409843039809312,-6.4713155981658));
#21579=CARTESIAN_POINT('Ctrl Pts',(95.2978654715237,0.500093500750323,-6.47710355914663));
#21580=CARTESIAN_POINT('Ctrl Pts',(95.3198421132795,0.548371911951468,-6.48020434912742));
#21581=CARTESIAN_POINT('Ctrl Pts',(95.3765892482316,0.654756327765499,-6.48724330232058));
#21582=CARTESIAN_POINT('Ctrl Pts',(95.413120951706,0.711732229437045,-6.49116523286909));
#21583=CARTESIAN_POINT('Ctrl Pts',(95.469531735161,0.785898167737987,-6.49681222101937));
#21584=CARTESIAN_POINT('Ctrl Pts',(95.485652209214,0.805807056419567,-6.49838835766165));
#21585=CARTESIAN_POINT('Ctrl Pts',(95.5023647968546,0.825211298936453,-6.49999999999997));
#21586=CARTESIAN_POINT('',(97.4187254286765,0.825062281452326,-6.49999885521441));
#21587=CARTESIAN_POINT('Origin',(96.460480949577,-1.62868768791465E-15,
-6.49999999999999));
#21588=CARTESIAN_POINT('Ctrl Pts',(97.4187254286765,0.825062281452326,-6.49999885521441));
#21589=CARTESIAN_POINT('Ctrl Pts',(97.3858967656753,0.863190172866516,-6.49681290469843));
#21590=CARTESIAN_POINT('Ctrl Pts',(97.3507105028266,0.899446588913635,-6.49362695418244));
#21591=CARTESIAN_POINT('Ctrl Pts',(97.3134115668534,0.933525367685571,-6.49044100366646));
#21592=CARTESIAN_POINT('Ctrl Pts',(97.2771416397765,0.966663975763241,-6.48734294765305));
#21593=CARTESIAN_POINT('Ctrl Pts',(97.2388745424285,0.997743144397279,-6.48424489163965));
#21594=CARTESIAN_POINT('Ctrl Pts',(97.1988758698889,1.0265150713251,-6.48114683562624));
#21595=CARTESIAN_POINT('Ctrl Pts',(97.1589169072214,1.05525843406648,-6.4780518553001));
#21596=CARTESIAN_POINT('Ctrl Pts',(97.1172302197181,1.08169876539954,-6.47495687497397));
#21597=CARTESIAN_POINT('Ctrl Pts',(97.0741146672841,1.1056282876686,-6.47186189464784));
#21598=CARTESIAN_POINT('Ctrl Pts',(97.0310230292357,1.12954453723697,-6.46876863097727));
#21599=CARTESIAN_POINT('Ctrl Pts',(96.9865045804255,1.15095246716872,-6.46567536730671));
#21600=CARTESIAN_POINT('Ctrl Pts',(96.9408850876952,1.16968889627921,-6.46258210363614));
#21601=CARTESIAN_POINT('Ctrl Pts',(96.8928974367663,1.18939795409635,-6.45932826523569));
#21602=CARTESIAN_POINT('Ctrl Pts',(96.8436918788377,1.20615022387415,-6.45607442683525));
#21603=CARTESIAN_POINT('Ctrl Pts',(96.7936713798052,1.21981325915255,-6.45282058843481));
#21604=CARTESIAN_POINT('Ctrl Pts',(96.7460773488615,1.23281350777867,-6.4497245920231));
#21605=CARTESIAN_POINT('Ctrl Pts',(96.6977462137278,1.24301728061555,-6.44662859561139));
#21606=CARTESIAN_POINT('Ctrl Pts',(96.6490372721396,1.25036265268188,-6.44353259919968));
#21607=CARTESIAN_POINT('Ctrl Pts',(96.6002978581226,1.2577126200303,-6.44043466592531));
#21608=CARTESIAN_POINT('Ctrl Pts',(96.5511807201814,1.26220058097111,-6.43733673265095));
#21609=CARTESIAN_POINT('Ctrl Pts',(96.5020493292532,1.26381656889404,-6.43423879937658));
#21610=CARTESIAN_POINT('Ctrl Pts',(96.4528335652593,1.26543533194407,-6.43113554603856));
#21611=CARTESIAN_POINT('Ctrl Pts',(96.4036040526838,1.26417230827103,-6.42803229270053));
#21612=CARTESIAN_POINT('Ctrl Pts',(96.3547213014283,1.26006950079092,-6.4249290393625));
#21613=CARTESIAN_POINT('Ctrl Pts',(96.347407095385,1.25945560778172,-6.42446470718527));
#21614=CARTESIAN_POINT('Ctrl Pts',(96.3401006350908,1.25877823000001,-6.42400037500805));
#21615=CARTESIAN_POINT('Ctrl Pts',(96.3328031071444,1.25803760617549,-6.42353604283083));
#21616=CARTESIAN_POINT('Ctrl Pts',(96.2836700641156,1.25305110903481,-6.4204097714399));
#21617=CARTESIAN_POINT('Ctrl Pts',(96.2347256224352,1.24517140652293,-6.41728350004898));
#21618=CARTESIAN_POINT('Ctrl Pts',(96.1863359402262,1.23442487169048,-6.41415722865805));
#21619=CARTESIAN_POINT('Ctrl Pts',(96.1380323097693,1.22369744750535,-6.41103651674011));
#21620=CARTESIAN_POINT('Ctrl Pts',(96.0902820109455,1.2101134209591,-6.40791580482216));
#21621=CARTESIAN_POINT('Ctrl Pts',(96.0434444403454,1.19375072773503,-6.40479509290421));
#21622=CARTESIAN_POINT('Ctrl Pts',(95.9966526848103,1.17740403999209,-6.40167743357028));
#21623=CARTESIAN_POINT('Ctrl Pts',(95.9507724029185,1.15828424662825,-6.39855977423634));
#21624=CARTESIAN_POINT('Ctrl Pts',(95.9061490746303,1.1365194333658,-6.39544211490241));
#21625=CARTESIAN_POINT('Ctrl Pts',(95.8615505829259,1.11476673402734,-6.39232619080451));
#21626=CARTESIAN_POINT('Ctrl Pts',(95.8182081485231,1.09037217084127,-6.3892102667066));
#21627=CARTESIAN_POINT('Ctrl Pts',(95.7764460648763,1.06351141343782,-6.3860943426087));
#21628=CARTESIAN_POINT('Ctrl Pts',(95.7346896203363,1.03665428302482,-6.38297883925198));
#21629=CARTESIAN_POINT('Ctrl Pts',(95.694513561082,1.00733191603579,-6.37986333589527));
#21630=CARTESIAN_POINT('Ctrl Pts',(95.6562141965028,0.975763926315942,-6.37674783253855));
#21631=CARTESIAN_POINT('Ctrl Pts',(95.6178768828815,0.9441646573573,-6.37362924217584));
#21632=CARTESIAN_POINT('Ctrl Pts',(95.5814203974895,0.910315672587025,-6.37051065181313));
#21633=CARTESIAN_POINT('Ctrl Pts',(95.5471074406779,0.87447646237127,-6.36739206145042));
#21634=CARTESIAN_POINT('Ctrl Pts',(95.5127753534812,0.838617270843461,-6.36427173239071));
#21635=CARTESIAN_POINT('Ctrl Pts',(95.4805895286139,0.800766060685597,-6.36115140333101));
#21636=CARTESIAN_POINT('Ctrl Pts',(95.4507729140603,0.761216088251567,-6.3580310742713));
#21637=CARTESIAN_POINT('Ctrl Pts',(95.4209015349594,0.721593473890639,-6.35490501406435));
#21638=CARTESIAN_POINT('Ctrl Pts',(95.3934083529415,0.680266325213899,-6.3517789538574));
#21639=CARTESIAN_POINT('Ctrl Pts',(95.3684725476981,0.637556193778903,-6.34865289365045));
#21640=CARTESIAN_POINT('Ctrl Pts',(95.3572992818796,0.618418586350414,-6.3472521648063));
#21641=CARTESIAN_POINT('Ctrl Pts',(95.3466388518098,0.599003620967653,-6.34585143596215));
#21642=CARTESIAN_POINT('Ctrl Pts',(95.3365042561199,0.57934155950119,-6.344450707118));
#21643=CARTESIAN_POINT('Ctrl Pts',(95.3139346980989,0.535554510598412,-6.34133130976981));
#21644=CARTESIAN_POINT('Ctrl Pts',(95.2938776347594,0.490349461827888,-6.33821191242163));
#21645=CARTESIAN_POINT('Ctrl Pts',(95.2765114333301,0.444045532122585,-6.33509251507345));
#21646=CARTESIAN_POINT('Ctrl Pts',(95.2591772324271,0.397826926207398,-6.33197886580769));
#21647=CARTESIAN_POINT('Ctrl Pts',(95.2445242506752,0.350513965059787,-6.32886521654193));
#21648=CARTESIAN_POINT('Ctrl Pts',(95.232684067834,0.302448453760651,-6.32575156727617));
#21649=CARTESIAN_POINT('Ctrl Pts',(95.220855913153,0.254431771071159,-6.32264108109264));
#21650=CARTESIAN_POINT('Ctrl Pts',(95.2118350314374,0.205664582037257,-6.31953059490911));
#21651=CARTESIAN_POINT('Ctrl Pts',(95.2057034563715,0.156504608701772,-6.31642010872558));
#21652=CARTESIAN_POINT('Ctrl Pts',(95.1995754915037,0.107373580171323,-6.31331145395916));
#21653=CARTESIAN_POINT('Ctrl Pts',(95.1963335310209,0.05785076914855,-6.31020279919274));
#21654=CARTESIAN_POINT('Ctrl Pts',(95.1960082049391,0.00830229292427632,
-6.30709414442632));
#21655=CARTESIAN_POINT('Ctrl Pts',(95.1956829314711,-0.0412381699983763,
-6.30398599241175));
#21656=CARTESIAN_POINT('Ctrl Pts',(95.1982733584799,-0.0908037412840867,
-6.30087784039718));
#21657=CARTESIAN_POINT('Ctrl Pts',(95.2037580231822,-0.140027626822785,
-6.29776968838261));
#21658=CARTESIAN_POINT('Ctrl Pts',(95.2092480204707,-0.189299371369654,
-6.29465851439871));
#21659=CARTESIAN_POINT('Ctrl Pts',(95.2176378114134,-0.238228220506546,
-6.29154734041481));
#21660=CARTESIAN_POINT('Ctrl Pts',(95.2288541630233,-0.286453676260998,
-6.2884361664309));
#21661=CARTESIAN_POINT('Ctrl Pts',(95.2400766117048,-0.334705346783249,
-6.28532330125088));
#21662=CARTESIAN_POINT('Ctrl Pts',(95.2541285246363,-0.382252335743913,
-6.28221043607086));
#21663=CARTESIAN_POINT('Ctrl Pts',(95.270886658549,-0.428748962393644,-6.27909757089083));
#21664=CARTESIAN_POINT('Ctrl Pts',(95.2876757185828,-0.475331395751545,
-6.27597896110667));
#21665=CARTESIAN_POINT('Ctrl Pts',(95.3071807497549,-0.520859093903896,
-6.2728603513225));
#21666=CARTESIAN_POINT('Ctrl Pts',(95.3292308904484,-0.56500756961433,-6.26974174153834));
#21667=CARTESIAN_POINT('Ctrl Pts',(95.3395452702353,-0.585658873015048,
-6.26828295149395));
#21668=CARTESIAN_POINT('Ctrl Pts',(95.3504158959013,-0.60600876625644,-6.26682416144957));
#21669=CARTESIAN_POINT('Ctrl Pts',(95.3618220279849,-0.626026216708281,
-6.26536537140518));
#21670=CARTESIAN_POINT('Ctrl Pts',(95.3862264404441,-0.668855294403235,
-6.26224416312234));
#21671=CARTESIAN_POINT('Ctrl Pts',(95.4131923737913,-0.710348849357345,
-6.25912295483949));
#21672=CARTESIAN_POINT('Ctrl Pts',(95.4425490824497,-0.75018328686182,-6.25600174655665));
#21673=CARTESIAN_POINT('Ctrl Pts',(95.4718610012655,-0.789956948541213,
-6.25288530033449));
#21674=CARTESIAN_POINT('Ctrl Pts',(95.5035561501367,-0.828076067984123,
-6.24976885411233));
#21675=CARTESIAN_POINT('Ctrl Pts',(95.5374191234865,-0.864243666574703,
-6.24665240789017));
#21676=CARTESIAN_POINT('Ctrl Pts',(95.5712482049335,-0.900375066668326,
-6.24353908077665));
#21677=CARTESIAN_POINT('Ctrl Pts',(95.6072404428918,-0.934558414240511,
-6.24042575366312));
#21678=CARTESIAN_POINT('Ctrl Pts',(95.6451400881149,-0.966529632049719,
-6.2373124265496));
#21679=CARTESIAN_POINT('Ctrl Pts',(95.6830156252808,-0.99848051288896,-6.23420107983107));
#21680=CARTESIAN_POINT('Ctrl Pts',(95.7227957457026,-1.02822170148917,-6.23108973311255));
#21681=CARTESIAN_POINT('Ctrl Pts',(95.7641896991281,-1.05552770903858,-6.22797838639403));
#21682=CARTESIAN_POINT('Ctrl Pts',(95.8055977453848,-1.0828430130897,-6.22486598039799));
#21683=CARTESIAN_POINT('Ctrl Pts',(95.8486202712027,-1.1077211674086,-6.22175357440194));
#21684=CARTESIAN_POINT('Ctrl Pts',(95.8929370890279,-1.12997974156752,-6.21864116840589));
#21685=CARTESIAN_POINT('Ctrl Pts',(95.9341181936383,-1.15066337175352,-6.21574898608768));
#21686=CARTESIAN_POINT('Ctrl Pts',(95.9764163061855,-1.16908529998863,-6.21285680376948));
#21687=CARTESIAN_POINT('Ctrl Pts',(96.019557376503,-1.18513571067102,-6.20996462145127));
#21688=CARTESIAN_POINT('Origin',(96.460480949577,-1.62868768791465E-15,
-6.49999999999999));
#21689=CARTESIAN_POINT('',(97.7249806670019,0.000845359370495013,-6.05658032632427));
#21690=CARTESIAN_POINT('Ctrl Pts',(96.019557376503,-1.18513571067102,-6.20996462145127));
#21691=CARTESIAN_POINT('Ctrl Pts',(96.0660267857944,-1.20242441254618,-6.20684930690527));
#21692=CARTESIAN_POINT('Ctrl Pts',(96.1134739318379,-1.21696085111713,-6.20373399235928));
#21693=CARTESIAN_POINT('Ctrl Pts',(96.161542157495,-1.22865611486231,-6.20061867781328));
#21694=CARTESIAN_POINT('Ctrl Pts',(96.2096996992633,-1.24037310970873,-6.19749757466625));
#21695=CARTESIAN_POINT('Ctrl Pts',(96.2584800847753,-1.24923829350367,-6.19437647151922));
#21696=CARTESIAN_POINT('Ctrl Pts',(96.3075178516391,-1.25521414135965,-6.19125536837219));
#21697=CARTESIAN_POINT('Ctrl Pts',(96.3335747928904,-1.25838949632519,-6.18959692414558));
#21698=CARTESIAN_POINT('Ctrl Pts',(96.3597043403319,-1.26074993511101,-6.18793847991896));
#21699=CARTESIAN_POINT('Ctrl Pts',(96.3858516941013,-1.26229581486558,-6.18628003569235));
#21700=CARTESIAN_POINT('Ctrl Pts',(96.435076212288,-1.26520605912065,-6.18315787967173));
#21701=CARTESIAN_POINT('Ctrl Pts',(96.4845785340075,-1.26523899914194,-6.18003572365111));
#21702=CARTESIAN_POINT('Ctrl Pts',(96.5339939915407,-1.2623613122483,-6.1769135676305));
#21703=CARTESIAN_POINT('Ctrl Pts',(96.5833194667269,-1.25948886543608,-6.17379709685374));
#21704=CARTESIAN_POINT('Ctrl Pts',(96.6325578489456,-1.25371633546162,-6.17068062607698));
#21705=CARTESIAN_POINT('Ctrl Pts',(96.6813427647009,-1.24506237137752,-6.16756415530021));
#21706=CARTESIAN_POINT('Ctrl Pts',(96.7300787368613,-1.23641708940561,-6.16445081113095));
#21707=CARTESIAN_POINT('Ctrl Pts',(96.7783616064132,-1.22489619169181,-6.16133746696168));
#21708=CARTESIAN_POINT('Ctrl Pts',(96.8258305919044,-1.21057006771655,-6.15822412279241));
#21709=CARTESIAN_POINT('Ctrl Pts',(96.8732721248406,-1.19625222891322,-6.15511257915144));
#21710=CARTESIAN_POINT('Ctrl Pts',(96.9199001827917,-1.17913253598975,-6.15200103551048));
#21711=CARTESIAN_POINT('Ctrl Pts',(96.965367188887,-1.15933176241982,-6.14888949186952));
#21712=CARTESIAN_POINT('Ctrl Pts',(97.0108272190594,-1.13953402684777,-6.14577842562723));
#21713=CARTESIAN_POINT('Ctrl Pts',(97.0551260495896,-1.11705624700979,-6.14266735938494));
#21714=CARTESIAN_POINT('Ctrl Pts',(97.0979366269534,-1.09206708098938,-6.13955629314265));
#21715=CARTESIAN_POINT('Ctrl Pts',(97.1407889975127,-1.0670535196637,-6.13644218976777));
#21716=CARTESIAN_POINT('Ctrl Pts',(97.18214974099,-1.03952395519453,-6.13332808639288));
#21717=CARTESIAN_POINT('Ctrl Pts',(97.2217185565937,-1.00969181221967,-6.130213983018));
#21718=CARTESIAN_POINT('Ctrl Pts',(97.2613090242038,-0.979843345133546,
-6.12709817560965));
#21719=CARTESIAN_POINT('Ctrl Pts',(97.2991051938811,-0.947690145919837,
-6.12398236820129));
#21720=CARTESIAN_POINT('Ctrl Pts',(97.3348405799922,-0.913485351114174,
-6.12086656079294));
#21721=CARTESIAN_POINT('Ctrl Pts',(97.3706416870465,-0.87921765027555,-6.11774502310366));
#21722=CARTESIAN_POINT('Ctrl Pts',(97.4043740742807,-0.842891225610397,
-6.11462348541437));
#21723=CARTESIAN_POINT('Ctrl Pts',(97.4358099246297,-0.804794160281114,
-6.11150194772509));
#21724=CARTESIAN_POINT('Ctrl Pts',(97.450268823739,-0.787271439634474,-6.11006619847657));
#21725=CARTESIAN_POINT('Ctrl Pts',(97.4642424724161,-0.769374560283098,
-6.10863044922805));
#21726=CARTESIAN_POINT('Ctrl Pts',(97.4777118314382,-0.751133532062002,
-6.10719469997953));
#21727=CARTESIAN_POINT('Ctrl Pts',(97.5071324118337,-0.711290386119013,
-6.10405865051165));
#21728=CARTESIAN_POINT('Ctrl Pts',(97.5342734560223,-0.669628381785422,
-6.10092260104378));
#21729=CARTESIAN_POINT('Ctrl Pts',(97.5589058189251,-0.626436793617297,
-6.0977865515759));
#21730=CARTESIAN_POINT('Ctrl Pts',(97.5834971366913,-0.583317175996531,
-6.09465572773659));
#21731=CARTESIAN_POINT('Ctrl Pts',(97.6055877889655,-0.538673489737358,
-6.09152490389727));
#21732=CARTESIAN_POINT('Ctrl Pts',(97.6249909763388,-0.492825169376669,
-6.08839408005796));
#21733=CARTESIAN_POINT('Ctrl Pts',(97.6443683868088,-0.447037757963643,
-6.08526741548083));
#21734=CARTESIAN_POINT('Ctrl Pts',(97.6610652036555,-0.400049382221009,
-6.08214075090371));
#21735=CARTESIAN_POINT('Ctrl Pts',(97.6749410183884,-0.352203054022458,
-6.07901408632658));
#21736=CARTESIAN_POINT('Ctrl Pts',(97.6888061404595,-0.304393596062708,
-6.07588983114792));
#21737=CARTESIAN_POINT('Ctrl Pts',(97.6998544203136,-0.255728014784932,
-6.07276557596926));
#21738=CARTESIAN_POINT('Ctrl Pts',(97.7079947697202,-0.206566014996665,
-6.06964132079059));
#21739=CARTESIAN_POINT('Ctrl Pts',(97.7161336663075,-0.157412789218061,
-6.06651762320205));
#21740=CARTESIAN_POINT('Ctrl Pts',(97.7213655669361,-0.10776385298261,-6.0633939256135));
#21741=CARTESIAN_POINT('Ctrl Pts',(97.7236506113726,-0.0579884084902515,
-6.06027022802495));
#21742=CARTESIAN_POINT('Ctrl Pts',(97.7245503558778,-0.0383891473287692,
-6.05904026081016));
#21743=CARTESIAN_POINT('Ctrl Pts',(97.7249937807201,-0.0187703344427737,
-6.05781029359537));
#21744=CARTESIAN_POINT('Ctrl Pts',(97.7249806670025,0.000845358472601678,
-6.05658032638057));
#21745=CARTESIAN_POINT('Ctrl Pts',(97.7249806670019,0.000845359370495876,
-6.05658032632427));
#21746=CARTESIAN_POINT('Ctrl Pts',(97.724942949461,0.0572637554750245,-6.05304271091496));
#21747=CARTESIAN_POINT('Ctrl Pts',(97.7211253245776,0.113535642676729,-6.04950509550565));
#21748=CARTESIAN_POINT('Ctrl Pts',(97.7136104799324,0.169194060626093,-6.04596748009634));
#21749=CARTESIAN_POINT('Ctrl Pts',(97.7060297300186,0.225340603502209,-6.04239883976166));
#21750=CARTESIAN_POINT('Ctrl Pts',(97.6946867557502,0.28086263516355,-6.03883019942699));
#21751=CARTESIAN_POINT('Ctrl Pts',(97.6797160394721,0.335299933743501,-6.03526155909232));
#21752=CARTESIAN_POINT('Ctrl Pts',(97.6697147066154,0.371667301397188,-6.03287749415044));
#21753=CARTESIAN_POINT('Ctrl Pts',(97.6580953183572,0.407550950286845,-6.03049342920857));
#21754=CARTESIAN_POINT('Ctrl Pts',(97.6449097088553,0.442819110014967,-6.02810936426669));
#21755=CARTESIAN_POINT('Ctrl Pts',(97.6276440753,0.489000298829028,-6.02498759794618));
#21756=CARTESIAN_POINT('Ctrl Pts',(97.6076357168921,0.534271180751997,-6.02186583162567));
#21757=CARTESIAN_POINT('Ctrl Pts',(97.5850016737362,0.578284870056729,-6.01874406530516));
#21758=CARTESIAN_POINT('Ctrl Pts',(97.5624089541461,0.622218202415255,-6.01562799847524));
#21759=CARTESIAN_POINT('Ctrl Pts',(97.5372003063184,0.664898411212142,-6.01251193164533));
#21760=CARTESIAN_POINT('Ctrl Pts',(97.5095409883672,0.705998077202455,-6.00939586481541));
#21761=CARTESIAN_POINT('Ctrl Pts',(97.4819094985138,0.747056392732514,-6.00628293306688));
#21762=CARTESIAN_POINT('Ctrl Pts',(97.4518325243324,0.786536861185324,-6.00317000131835));
#21763=CARTESIAN_POINT('Ctrl Pts',(97.4195203777163,0.824138110558106,-6.00005706956981));
#21764=CARTESIAN_POINT('Ctrl Pts',(97.3872270000227,0.861717518765506,-5.9969459460074));
#21765=CARTESIAN_POINT('Ctrl Pts',(97.3527013785607,0.897419455662145,-5.99383482244498));
#21766=CARTESIAN_POINT('Ctrl Pts',(97.3161945573899,0.930975011159725,-5.99072369888257));
#21767=CARTESIAN_POINT('Ctrl Pts',(97.2796934185691,0.96452534367694,-5.98761305957193));
#21768=CARTESIAN_POINT('Ctrl Pts',(97.2412120962563,0.995929588346935,-5.98450242026129));
#21769=CARTESIAN_POINT('Ctrl Pts',(97.201037118162,1.02495698015608,-5.98139178095065));
#21770=CARTESIAN_POINT('Ctrl Pts',(97.1608230043676,1.05401264845363,-5.97827811146916));
#21771=CARTESIAN_POINT('Ctrl Pts',(97.118912386629,1.08068652087937,-5.97516444198767));
#21772=CARTESIAN_POINT('Ctrl Pts',(97.0756219020843,1.10479041385615,-5.97205077250619));
#21773=CARTESIAN_POINT('Ctrl Pts',(97.0323077895788,1.12890746274567,-5.96893540358287));
#21774=CARTESIAN_POINT('Ctrl Pts',(96.9876128046395,1.15045150098152,-5.96582003465955));
#21775=CARTESIAN_POINT('Ctrl Pts',(96.9418762119936,1.16928133967957,-5.96270466573624));
#21776=CARTESIAN_POINT('Ctrl Pts',(96.8960555227066,1.18814580111831,-5.95958356853175));
#21777=CARTESIAN_POINT('Ctrl Pts',(96.8491899218098,1.2042859250473,-5.95646247132727));
#21778=CARTESIAN_POINT('Ctrl Pts',(96.8016349782304,1.21761002736243,-5.95334137412279));
#21779=CARTESIAN_POINT('Ctrl Pts',(96.7797077400948,1.22375367389878,-5.95190225893315));
#21780=CARTESIAN_POINT('Ctrl Pts',(96.7576340950581,1.22929933041793,-5.95046314374352));
#21781=CARTESIAN_POINT('Ctrl Pts',(96.7354494469325,1.23424170058463,-5.94902402855388));
#21782=CARTESIAN_POINT('Ctrl Pts',(96.687325890964,1.24496282746424,-5.94590225984332));
#21783=CARTESIAN_POINT('Ctrl Pts',(96.6384691452877,1.2528886495232,-5.94278049113275));
#21784=CARTESIAN_POINT('Ctrl Pts',(96.5892337875813,1.25792804114776,-5.93965872242218));
#21785=CARTESIAN_POINT('Ctrl Pts',(96.5400882948944,1.26295823480874,-5.93654265160474));
#21786=CARTESIAN_POINT('Ctrl Pts',(96.4905661015313,1.26511239186726,-5.93342658078729));
#21787=CARTESIAN_POINT('Ctrl Pts',(96.4410317718191,1.26435041799516,-5.93031050996984));
#21788=CARTESIAN_POINT('Ctrl Pts',(96.391547262928,1.26358921050395,-5.92719757324562));
#21789=CARTESIAN_POINT('Ctrl Pts',(96.3420511871433,1.25991768706299,-5.92408463652139));
#21790=CARTESIAN_POINT('Ctrl Pts',(96.2929108537378,1.25334772229435,-5.92097169979716));
#21791=CARTESIAN_POINT('Ctrl Pts',(96.2437990486393,1.24678157170357,-5.91786057028115));
#21792=CARTESIAN_POINT('Ctrl Pts',(96.1950431188634,1.23732038594117,-5.91474944076514));
#21793=CARTESIAN_POINT('Ctrl Pts',(96.1470053850065,1.22502788556717,-5.91163831124912));
#21794=CARTESIAN_POINT('Ctrl Pts',(96.0989751133304,1.21273729471001,-5.90852766501593));
#21795=CARTESIAN_POINT('Ctrl Pts',(96.0516633463213,1.19761639932997,-5.90541701878273));
#21796=CARTESIAN_POINT('Ctrl Pts',(96.0054197897736,1.17977946703543,-5.90230637254954));
#21797=CARTESIAN_POINT('Ctrl Pts',(95.9591311650348,1.16192515116717,-5.89919269473293));
#21798=CARTESIAN_POINT('Ctrl Pts',(95.9139133408995,1.14134971247037,-5.89607901691631));
#21799=CARTESIAN_POINT('Ctrl Pts',(95.8700967587827,1.1182158813307,-5.8929653390997));
#21800=CARTESIAN_POINT('Ctrl Pts',(95.8262562500839,1.09506941767883,-5.88984996102113));
#21801=CARTESIAN_POINT('Ctrl Pts',(95.7838189760765,1.06936206392372,-5.88673458294256));
#21802=CARTESIAN_POINT('Ctrl Pts',(95.7430883335839,1.04130114977296,-5.88361920486399));
#21803=CARTESIAN_POINT('Ctrl Pts',(95.7022827840257,1.01318862924908,-5.88049809734401));
#21804=CARTESIAN_POINT('Ctrl Pts',(95.6631905617938,0.982714247378316,-5.87737698982404));
#21805=CARTESIAN_POINT('Ctrl Pts',(95.6260824662031,0.950126002666643,-5.87425588230406));
#21806=CARTESIAN_POINT('Ctrl Pts',(95.6089728688084,0.935100393350445,-5.87281681914972));
#21807=CARTESIAN_POINT('Ctrl Pts',(95.5922845603638,0.919625915480621,-5.87137775599538));
#21808=CARTESIAN_POINT('Ctrl Pts',(95.5760412892255,0.903729349527431,-5.86993869284105));
#21809=CARTESIAN_POINT('Ctrl Pts',(95.5408058308823,0.86924597590934,-5.86681702791309));
#21810=CARTESIAN_POINT('Ctrl Pts',(95.5075130071989,0.83262338358838,-5.86369536298514));
#21811=CARTESIAN_POINT('Ctrl Pts',(95.476432611124,0.794109008630289,-5.86057369805718));
#21812=CARTESIAN_POINT('Ctrl Pts',(95.4454089666294,0.755664959405491,-5.85745773316656));
#21813=CARTESIAN_POINT('Ctrl Pts',(95.416590078647,0.715336401819541,-5.85434176827594));
#21814=CARTESIAN_POINT('Ctrl Pts',(95.3902084202193,0.673406981625764,-5.85122580338532));
#21815=CARTESIAN_POINT('Ctrl Pts',(95.363853307394,0.631519751414812,-5.84811297382317));
#21816=CARTESIAN_POINT('Ctrl Pts',(95.3399308595048,0.588035309205129,-5.84500014426103));
#21817=CARTESIAN_POINT('Ctrl Pts',(95.3186314929228,0.543267952615101,-5.84188731469889));
#21818=CARTESIAN_POINT('Ctrl Pts',(95.2973444990861,0.49852660126295,-5.83877629337112));
#21819=CARTESIAN_POINT('Ctrl Pts',(95.2786778027759,0.452504305890089,-5.83566527204336));
#21820=CARTESIAN_POINT('Ctrl Pts',(95.2627756474578,0.405539466976549,-5.8325542507156));
#21821=CARTESIAN_POINT('Ctrl Pts',(95.2468759666513,0.358581936194128,-5.82944371348939));
#21822=CARTESIAN_POINT('Ctrl Pts',(95.2337401473019,0.310682672174865,-5.82633317626319));
#21823=CARTESIAN_POINT('Ctrl Pts',(95.2234631880207,0.262197077776006,-5.82322263903698));
#21824=CARTESIAN_POINT('Ctrl Pts',(95.2131762138703,0.213664234295621,-5.82010907060061));
#21825=CARTESIAN_POINT('Ctrl Pts',(95.2057537744342,0.164544457014021,-5.81699550216423));
#21826=CARTESIAN_POINT('Ctrl Pts',(95.2012397426371,0.115203440679689,-5.81388193372785));
#21827=CARTESIAN_POINT('Ctrl Pts',(95.1967232463436,0.0658354859542773,
-5.81076666539694));
#21828=CARTESIAN_POINT('Ctrl Pts',(95.1951183372384,0.0162465998345455,
-5.80765139706602));
#21829=CARTESIAN_POINT('Ctrl Pts',(95.1964167562349,-0.0331958598393275,
-5.80453612873511));
#21830=CARTESIAN_POINT('Ctrl Pts',(95.1977175635096,-0.0827292626881025,
-5.80141513026062));
#21831=CARTESIAN_POINT('Ctrl Pts',(95.2019323095765,-0.132115155493617,
-5.79829413178612));
#21832=CARTESIAN_POINT('Ctrl Pts',(95.2090008683741,-0.180991315682097,
-5.79517313331163));
#21833=CARTESIAN_POINT('Ctrl Pts',(95.2122620674417,-0.203541158245179,
-5.79373320791717));
#21834=CARTESIAN_POINT('Ctrl Pts',(95.2161300120375,-0.225982649975628,
-5.7922932825227));
#21835=CARTESIAN_POINT('Ctrl Pts',(95.2205951934307,-0.248281214967158,
-5.79085335712823));
#21836=CARTESIAN_POINT('Ctrl Pts',(95.230275754311,-0.296624741675626,-5.7877315835167));
#21837=CARTESIAN_POINT('Ctrl Pts',(95.2428091104538,-0.344506970635032,
-5.78460980990517));
#21838=CARTESIAN_POINT('Ctrl Pts',(95.2581350348987,-0.391566790543403,
-5.78148803629364));
#21839=CARTESIAN_POINT('Ctrl Pts',(95.2734329771468,-0.438540688251809,
-5.77837196244162));
#21840=CARTESIAN_POINT('Ctrl Pts',(95.29151320669,-0.484694638242805,-5.77525588858961));
#21841=CARTESIAN_POINT('Ctrl Pts',(95.3122647913799,-0.529679057595407,
-5.7721398147376));
#21842=CARTESIAN_POINT('Ctrl Pts',(95.33299549677,-0.574618215673058,-5.76902687613724));
#21843=CARTESIAN_POINT('Ctrl Pts',(95.356392007711,-0.618389677535496,-5.76591393753689));
#21844=CARTESIAN_POINT('Ctrl Pts',(95.3822947611965,-0.660662389716154,
-5.76280099893653));
#21845=CARTESIAN_POINT('Ctrl Pts',(95.4081824672949,-0.702910544899029,
-5.7596898686996));
#21846=CARTESIAN_POINT('Ctrl Pts',(95.4365732457597,-0.743661208963535,
-5.75657873846266));
#21847=CARTESIAN_POINT('Ctrl Pts',(95.4672621461119,-0.782608879609272,
-5.75346760822573));
#21848=CARTESIAN_POINT('Ctrl Pts',(95.4979462678733,-0.821550485685259,
-5.75035696242511));
#21849=CARTESIAN_POINT('Ctrl Pts',(95.5309274612286,-0.858689226303311,
-5.7472463166245));
#21850=CARTESIAN_POINT('Ctrl Pts',(95.5659596632987,-0.893751597702029,
-5.74413567082388));
#21851=CARTESIAN_POINT('Ctrl Pts',(95.6010259877152,-0.928848120833089,
-5.74102199516709));
#21852=CARTESIAN_POINT('Ctrl Pts',(95.6381469203801,-0.961863849577999,
-5.73790831951029));
#21853=CARTESIAN_POINT('Ctrl Pts',(95.6770398840342,-0.992562515321442,
-5.73479464385349));
#21854=CARTESIAN_POINT('Ctrl Pts',(95.7159540733096,-1.02327793469302,-5.73167926892531));
#21855=CARTESIAN_POINT('Ctrl Pts',(95.7566417695088,-1.0516734592561,-5.72856389399714));
#21856=CARTESIAN_POINT('Ctrl Pts',(95.7987905632667,-1.07755560537013,-5.72544851906896));
#21857=CARTESIAN_POINT('Ctrl Pts',(95.8410168522527,-1.10348533867793,-5.72232741617875));
#21858=CARTESIAN_POINT('Ctrl Pts',(95.8847091167622,-1.12689221264401,-5.71920631328853));
#21859=CARTESIAN_POINT('Ctrl Pts',(95.9295309575404,-1.14762901495052,-5.71608521039832));
#21860=CARTESIAN_POINT('Ctrl Pts',(95.9501971946589,-1.15719023925783,-5.71464614740402));
#21861=CARTESIAN_POINT('Ctrl Pts',(95.9711033049277,-1.16618451330883,-5.71320708440971));
#21862=CARTESIAN_POINT('Ctrl Pts',(95.9922151859794,-1.17460096400538,-5.71176802141541));
#21863=CARTESIAN_POINT('Ctrl Pts',(96.0012843060533,-1.17821645434352,-5.71114983703585));
#21864=CARTESIAN_POINT('Ctrl Pts',(96.01039921241,-1.18172846338418,-5.7105316526563));
#21865=CARTESIAN_POINT('Ctrl Pts',(96.019557376503,-1.18513571067102,-5.70991346827675));
#21866=CARTESIAN_POINT('Ctrl Pts',(96.0195573766758,-1.18513571073528,-5.84684438197146));
#21867=CARTESIAN_POINT('Ctrl Pts',(95.9377838466584,-1.15471229449914,-5.85184356523696));
#21868=CARTESIAN_POINT('Ctrl Pts',(95.8593871237074,-1.11591032677119,-5.85675766807886));
#21869=CARTESIAN_POINT('Ctrl Pts',(95.7666978890307,-1.05741469043846,-5.8634180233614));
#21870=CARTESIAN_POINT('Ctrl Pts',(95.7480997743689,-1.04497545225213,-5.86480253184938));
#21871=CARTESIAN_POINT('Ctrl Pts',(95.7109005660367,-1.01864033194169,-5.86769259545907));
#21872=CARTESIAN_POINT('Ctrl Pts',(95.6923328699123,-1.00471250834484,-5.86919957672916));
#21873=CARTESIAN_POINT('Ctrl Pts',(95.6261344841347,-0.952148598586737,
-5.87478053896405));
#21874=CARTESIAN_POINT('Ctrl Pts',(95.5809499334651,-0.910573991331859,
-5.87899390296784));
#21875=CARTESIAN_POINT('Ctrl Pts',(95.4774791070059,-0.800455833223651,
-5.88938625455785));
#21876=CARTESIAN_POINT('Ctrl Pts',(95.4231293829763,-0.728648634844923,
-5.89552426270106));
#21877=CARTESIAN_POINT('Ctrl Pts',(95.3582414461938,-0.620750264390375,
-5.90372158879092));
#21878=CARTESIAN_POINT('Ctrl Pts',(95.3409726780465,-0.589036907625956,
-5.90602447030197));
#21879=CARTESIAN_POINT('Ctrl Pts',(95.3087872286146,-0.52338538632302,-5.91059300222629));
#21880=CARTESIAN_POINT('Ctrl Pts',(95.2939579424961,-0.489443754131257,
-5.91285390519707));
#21881=CARTESIAN_POINT('Ctrl Pts',(95.2660535381213,-0.417069615502774,
-5.91750072706743));
#21882=CARTESIAN_POINT('Ctrl Pts',(95.2532957123027,-0.378560547984007,
-5.91987519370583));
#21883=CARTESIAN_POINT('Ctrl Pts',(95.2172438834632,-0.249213356459102,
-5.92764290854262));
#21884=CARTESIAN_POINT('Ctrl Pts',(95.2021975041997,-0.156414919864184,
-5.93286805880145));
#21885=CARTESIAN_POINT('Ctrl Pts',(95.1961020405665,-0.0338615463724993,
-5.94015787448968));
#21886=CARTESIAN_POINT('Ctrl Pts',(95.1956581871163,-0.00486958004534194,
-5.94191245365027));
#21887=CARTESIAN_POINT('Ctrl Pts',(95.1965952834404,0.0442708302043974,
-5.94497541410896));
#21888=CARTESIAN_POINT('Ctrl Pts',(95.197461846205,0.0644161774360809,-5.94625847331155));
#21889=CARTESIAN_POINT('Ctrl Pts',(95.2012630394973,0.121150615412437,-5.94994548629421));
#21890=CARTESIAN_POINT('Ctrl Pts',(95.2053093715755,0.157642023163297,-5.95239915052863));
#21891=CARTESIAN_POINT('Ctrl Pts',(95.2204363873285,0.255123649668902,-5.95909101875221));
#21892=CARTESIAN_POINT('Ctrl Pts',(95.2344229438567,0.315563431192348,-5.96338255967212));
#21893=CARTESIAN_POINT('Ctrl Pts',(95.2727827406317,0.439189877247954,-5.9722399254486));
#21894=CARTESIAN_POINT('Ctrl Pts',(95.2979127922853,0.501948616771625,-5.97677995814351));
#21895=CARTESIAN_POINT('Ctrl Pts',(95.3436918443134,0.594135635105346,-5.98345564412554));
#21896=CARTESIAN_POINT('Ctrl Pts',(95.3607743043712,0.625188582668533,-5.98570740020361));
#21897=CARTESIAN_POINT('Ctrl Pts',(95.3989251941076,0.688125293286197,-5.99029053299647));
#21898=CARTESIAN_POINT('Ctrl Pts',(95.4201794543918,0.71985435728773,-5.99261207810089));
#21899=CARTESIAN_POINT('Ctrl Pts',(95.468313267508,0.785114926358987,-5.997450063231));
#21900=CARTESIAN_POINT('Ctrl Pts',(95.4955311572602,0.818336401419655,-5.99995141032774));
#21901=CARTESIAN_POINT('Ctrl Pts',(95.5819243249958,0.91346759310317,-6.00735903496852));
#21902=CARTESIAN_POINT('Ctrl Pts',(95.6457396576691,0.97081369771625,-6.0121541974527));
#21903=CARTESIAN_POINT('Ctrl Pts',(95.7390211249825,1.03891846894308,-6.01900113372312));
#21904=CARTESIAN_POINT('Ctrl Pts',(95.763808204436,1.05570006645382,-6.02080853851395));
#21905=CARTESIAN_POINT('Ctrl Pts',(95.8062295325529,1.08227576279618,-6.02392352745981));
#21906=CARTESIAN_POINT('Ctrl Pts',(95.8235436910789,1.09255503491885,-6.02520255811905));
#21907=CARTESIAN_POINT('Ctrl Pts',(95.8719328175188,1.1197421330204,-6.02879632178875));
#21908=CARTESIAN_POINT('Ctrl Pts',(95.9034804230934,1.13576462552936,-6.03115591766485));
#21909=CARTESIAN_POINT('Ctrl Pts',(95.9880121159412,1.17432757435207,-6.0374468266035));
#21910=CARTESIAN_POINT('Ctrl Pts',(96.0419377967847,1.19461016973284,-6.04142594787677));
#21911=CARTESIAN_POINT('Ctrl Pts',(96.1671680275022,1.23218750924559,-6.05038958391888));
#21912=CARTESIAN_POINT('Ctrl Pts',(96.2389831311708,1.24710070499728,-6.05533117020251));
#21913=CARTESIAN_POINT('Ctrl Pts',(96.3469719648906,1.25989599374294,-6.06238661115841));
#21914=CARTESIAN_POINT('Ctrl Pts',(96.3824122021595,1.26258777491013,-6.0646455922689));
#21915=CARTESIAN_POINT('Ctrl Pts',(96.455951841438,1.26506428838531,-6.06922918432197));
#21916=CARTESIAN_POINT('Ctrl Pts',(96.4940227306363,1.26462783763334,-6.07154456956882));
#21917=CARTESIAN_POINT('Ctrl Pts',(96.5745983377002,1.26006201217088,-6.07636138045156));
#21918=CARTESIAN_POINT('Ctrl Pts',(96.6170303053683,1.25549661871334,-6.07884816573145));
#21919=CARTESIAN_POINT('Ctrl Pts',(96.7470579101663,1.23481042456195,-6.08643997120845));
#21920=CARTESIAN_POINT('Ctrl Pts',(96.8332323465718,1.211584461685,-6.09141822937776));
#21921=CARTESIAN_POINT('Ctrl Pts',(96.9428302335981,1.16923549102459,-6.09840733162763));
#21922=CARTESIAN_POINT('Ctrl Pts',(96.9690569000964,1.15806851391745,-6.10013441287575));
#21923=CARTESIAN_POINT('Ctrl Pts',(97.0131263763159,1.13751858671315,-6.10316734832646));
#21924=CARTESIAN_POINT('Ctrl Pts',(97.0311617532308,1.12857819228048,-6.1044494106973));
#21925=CARTESIAN_POINT('Ctrl Pts',(97.0818731551988,1.10191353999248,-6.10816764326997));
#21926=CARTESIAN_POINT('Ctrl Pts',(97.1139890613338,1.08317511718216,-6.11065552838991));
#21927=CARTESIAN_POINT('Ctrl Pts',(97.1987493423038,1.02857804891638,-6.11750267408036));
#21928=CARTESIAN_POINT('Ctrl Pts',(97.2495884526673,0.990112297282799,-6.12191768364368));
#21929=CARTESIAN_POINT('Ctrl Pts',(97.3464868594598,0.90457495238809,-6.13075922085882));
#21930=CARTESIAN_POINT('Ctrl Pts',(97.3922129356389,0.857403063605749,-6.13516772027039));
#21931=CARTESIAN_POINT('Ctrl Pts',(97.4565573496004,0.779764804595199,-6.14170750247376));
#21932=CARTESIAN_POINT('Ctrl Pts',(97.477895688305,0.751710716185097,-6.14394683067393));
#21933=CARTESIAN_POINT('Ctrl Pts',(97.5197265934111,0.691663803997951,-6.14850393876889));
#21934=CARTESIAN_POINT('Ctrl Pts',(97.5400058417601,0.659565469658199,-6.15081201112935));
#21935=CARTESIAN_POINT('Ctrl Pts',(97.5799267063304,0.589590556856843,-6.15561839570102));
#21936=CARTESIAN_POINT('Ctrl Pts',(97.5991580455471,0.551534862638533,-6.15810190201137));
#21937=CARTESIAN_POINT('Ctrl Pts',(97.6511395788588,0.434307741591374,-6.16549311347615));
#21938=CARTESIAN_POINT('Ctrl Pts',(97.6778046639425,0.352720868597642,-6.1702873132448));
#21939=CARTESIAN_POINT('Ctrl Pts',(97.7024407616585,0.239595895572774,-6.17714447244319));
#21940=CARTESIAN_POINT('Ctrl Pts',(97.7078027341326,0.209900946158523,-6.17896487835704));
#21941=CARTESIAN_POINT('Ctrl Pts',(97.7149602514241,0.16014426766828,-6.18209117907099));
#21942=CARTESIAN_POINT('Ctrl Pts',(97.7173474675812,0.140181650018631,-6.18336751754647));
#21943=CARTESIAN_POINT('Ctrl Pts',(97.7225664287677,0.0855135013051155,
-6.18692143025161));
#21944=CARTESIAN_POINT('Ctrl Pts',(97.724442004365,0.0507376283597556,-6.18924197574226));
#21945=CARTESIAN_POINT('Ctrl Pts',(97.7255820254749,-0.0397354676565079,
-6.19536405909827));
#21946=CARTESIAN_POINT('Ctrl Pts',(97.7226063916071,-0.0953872984476596,
-6.19921099590677));
#21947=CARTESIAN_POINT('Ctrl Pts',(97.7068658677574,-0.226557147900269,
-6.20827732408373));
#21948=CARTESIAN_POINT('Ctrl Pts',(97.6908937181905,-0.301481694010448,
-6.21344744300113));
#21949=CARTESIAN_POINT('Ctrl Pts',(97.6576854221984,-0.408574855025839,
-6.22072325557859));
#21950=CARTESIAN_POINT('Ctrl Pts',(97.6456866098355,-0.442176346821572,
-6.22299125162701));
#21951=CARTESIAN_POINT('Ctrl Pts',(97.617888710023,-0.510719390393977,-6.22759943193466));
#21952=CARTESIAN_POINT('Ctrl Pts',(97.6018893822474,-0.545540344791768,
-6.22993004210697));
#21953=CARTESIAN_POINT('Ctrl Pts',(97.5646035255323,-0.617840052266742,
-6.23478583766901));
#21954=CARTESIAN_POINT('Ctrl Pts',(97.5429330567653,-0.655065524087496,
-6.23729592838875));
#21955=CARTESIAN_POINT('Ctrl Pts',(97.4726103156454,-0.762813743163785,
-6.24471738087989));
#21956=CARTESIAN_POINT('Ctrl Pts',(97.4186589182231,-0.829568245543577,
-6.24951843919097));
#21957=CARTESIAN_POINT('Ctrl Pts',(97.3373178329375,-0.91159879349207,-6.25637095018362));
#21958=CARTESIAN_POINT('Ctrl Pts',(97.3155072984659,-0.932086318659482,
-6.25817867576091));
#21959=CARTESIAN_POINT('Ctrl Pts',(97.2776214913067,-0.965224658932037,
-6.26131178079223));
#21960=CARTESIAN_POINT('Ctrl Pts',(97.2619296914768,-0.978292919070695,
-6.26260962424126));
#21961=CARTESIAN_POINT('Ctrl Pts',(97.2166900299023,-1.01414991250018,-6.26634822695243));
#21962=CARTESIAN_POINT('Ctrl Pts',(97.1864425977976,-1.0360170729478,-6.26883956726225));
#21963=CARTESIAN_POINT('Ctrl Pts',(97.1015948146238,-1.09181555285675,-6.2757169391872));
#21964=CARTESIAN_POINT('Ctrl Pts',(97.045301538233,-1.12297512068837,-6.28015755047713));
#21965=CARTESIAN_POINT('Ctrl Pts',(96.9301258788272,-1.17570859017423,-6.28878601985194));
#21966=CARTESIAN_POINT('Ctrl Pts',(96.8715153220139,-1.19745966678565,-6.292965596508));
#21967=CARTESIAN_POINT('Ctrl Pts',(96.7773748366626,-1.22466425812783,-6.29931090150239));
#21968=CARTESIAN_POINT('Ctrl Pts',(96.7428156740292,-1.23309034363115,-6.30156745581243));
#21969=CARTESIAN_POINT('Ctrl Pts',(96.6699170171589,-1.24763794538777,-6.30618972399131));
#21970=CARTESIAN_POINT('Ctrl Pts',(96.6315583150243,-1.25347393923124,-6.30854417833269));
#21971=CARTESIAN_POINT('Ctrl Pts',(96.5492967749851,-1.26214190166454,-6.31346999376593));
#21972=CARTESIAN_POINT('Ctrl Pts',(96.505392398636,-1.26446582306308,-6.31602491438671));
#21973=CARTESIAN_POINT('Ctrl Pts',(96.3760774890712,-1.26456530719757,-6.32346611019265));
#21974=CARTESIAN_POINT('Ctrl Pts',(96.2909218307323,-1.25598436430066,-6.32824871607656));
#21975=CARTESIAN_POINT('Ctrl Pts',(96.1785977465977,-1.23302863673213,-6.33505754105091));
#21976=CARTESIAN_POINT('Ctrl Pts',(96.150122379193,-1.22617087271748,-6.33682981368999));
#21977=CARTESIAN_POINT('Ctrl Pts',(96.1031907638755,-1.21312883842954,-6.3398668267478));
#21978=CARTESIAN_POINT('Ctrl Pts',(96.0845945013905,-1.20749621547019,-6.34110276829313));
#21979=CARTESIAN_POINT('Ctrl Pts',(96.0505020436517,-1.19630608524143,-6.34343061982689));
#21980=CARTESIAN_POINT('Ctrl Pts',(96.0349733858114,-1.1908711566551,-6.34451408366555));
#21981=CARTESIAN_POINT('Ctrl Pts',(96.0195573796018,-1.18513571182389,-6.34560991122238));
#21982=CARTESIAN_POINT('Origin',(96.460480949577,-1.76391462320204E-15,
-7.60421172358872));
#21983=CARTESIAN_POINT('',(98.0034803719728,-0.00133509777570635,-5.85421172355731));
#21984=CARTESIAN_POINT('Ctrl Pts',(95.5205266553345,1.22365637526844,-6.17704955921195));
#21985=CARTESIAN_POINT('Ctrl Pts',(95.4750360039568,1.18871263291183,-6.17408432509521));
#21986=CARTESIAN_POINT('Ctrl Pts',(95.431424748673,1.15117353037341,-6.17111909097847));
#21987=CARTESIAN_POINT('Ctrl Pts',(95.3900012076878,1.11127049911566,-6.16815385686173));
#21988=CARTESIAN_POINT('Ctrl Pts',(95.3486178575488,1.07140618344223,-6.16519149973874));
#21989=CARTESIAN_POINT('Ctrl Pts',(95.309418389521,1.02918284333066,-6.16222914261575));
#21990=CARTESIAN_POINT('Ctrl Pts',(95.2726777313522,0.984871826571724,-6.15926678549276));
#21991=CARTESIAN_POINT('Ctrl Pts',(95.2359585877192,0.940586757387131,-6.15630616306211));
#21992=CARTESIAN_POINT('Ctrl Pts',(95.2016957315978,0.894216835472797,-6.15334554063147));
#21993=CARTESIAN_POINT('Ctrl Pts',(95.1701253722669,0.846068250263889,-6.15038491820082));
#21994=CARTESIAN_POINT('Ctrl Pts',(95.1385613565695,0.797929339857214,-6.14742489066692));
#21995=CARTESIAN_POINT('Ctrl Pts',(95.109689048867,0.748012911522314,-6.14446486313301));
#21996=CARTESIAN_POINT('Ctrl Pts',(95.0837014019618,0.696654202074729,-6.14150483559911));
#21997=CARTESIAN_POINT('Ctrl Pts',(95.057689999433,0.645248545007449,-6.13854210226811));
#21998=CARTESIAN_POINT('Ctrl Pts',(95.0345687627803,0.592398438366997,-6.13557936893711));
#21999=CARTESIAN_POINT('Ctrl Pts',(95.0144840397897,0.538462567766447,-6.13261663560611));
#22000=CARTESIAN_POINT('Ctrl Pts',(94.9943905569729,0.484503173373546,-6.12965261009752));
#22001=CARTESIAN_POINT('Ctrl Pts',(94.9773363829618,0.429457569615514,-6.12668858458892));
#22002=CARTESIAN_POINT('Ctrl Pts',(94.9634180905899,0.373700142148047,-6.12372455908032));
#22003=CARTESIAN_POINT('Ctrl Pts',(94.9494732659501,0.317836424988612,-6.12075488328669));
#22004=CARTESIAN_POINT('Ctrl Pts',(94.9386763655485,0.261258686260434,-6.11778520749305));
#22005=CARTESIAN_POINT('Ctrl Pts',(94.9310726844337,0.204351066822466,-6.11481553169941));
#22006=CARTESIAN_POINT('Ctrl Pts',(94.9245684531917,0.155671971700926,-6.11227525445945));
#22007=CARTESIAN_POINT('Ctrl Pts',(94.920399894136,0.106751803719814,-6.10973497721949));
#22008=CARTESIAN_POINT('Ctrl Pts',(94.9185650739381,0.0578310682319644,
-6.10719469997953));
#22009=CARTESIAN_POINT('Ctrl Pts',(94.9164199209303,0.000636110926563641,
-6.10422477226208));
#22010=CARTESIAN_POINT('Ctrl Pts',(94.9174569443836,-0.0567975521573849,
-6.10125484454463));
#22011=CARTESIAN_POINT('Ctrl Pts',(94.921704385593,-0.114086310017802,-6.09828491682718));
#22012=CARTESIAN_POINT('Ctrl Pts',(94.9259443171463,-0.171273778927885,
-6.09532024006772));
#22013=CARTESIAN_POINT('Ctrl Pts',(94.9333833618724,-0.228316335375274,
-6.09235556330827));
#22014=CARTESIAN_POINT('Ctrl Pts',(94.9439977754811,-0.284829392240432,
-6.08939088654881));
#22015=CARTESIAN_POINT('Ctrl Pts',(94.9546017033752,-0.341286621265306,
-6.08642913851963));
#22016=CARTESIAN_POINT('Ctrl Pts',(94.9683746892567,-0.397214877187807,
-6.08346739049045));
#22017=CARTESIAN_POINT('Ctrl Pts',(94.9852412891601,-0.452235496542447,
-6.08050564246127));
#22018=CARTESIAN_POINT('Ctrl Pts',(95.0020977234071,-0.507222954458717,
-6.07754567950514));
#22019=CARTESIAN_POINT('Ctrl Pts',(95.0220439230071,-0.561303362708368,
-6.07458571654901));
#22020=CARTESIAN_POINT('Ctrl Pts',(95.044954050569,-0.61411122623253,-6.07162575359288));
#22021=CARTESIAN_POINT('Ctrl Pts',(95.0678591936993,-0.666907600637633,
-6.06866643461976));
#22022=CARTESIAN_POINT('Ctrl Pts',(95.0937267770205,-0.718431501928402,
-6.06570711564663));
#22023=CARTESIAN_POINT('Ctrl Pts',(95.1223829126007,-0.768337584295006,
-6.06274779667351));
#22024=CARTESIAN_POINT('Ctrl Pts',(95.1510648986118,-0.818288686469972,
-6.05978580812652));
#22025=CARTESIAN_POINT('Ctrl Pts',(95.1825402040583,-0.866618599759192,
-6.05682381957954));
#22026=CARTESIAN_POINT('Ctrl Pts',(95.2165897224079,-0.913008003782919,
-6.05386183103255));
#22027=CARTESIAN_POINT('Ctrl Pts',(95.2506536148954,-0.959416991275864,
-6.05089859207046));
#22028=CARTESIAN_POINT('Ctrl Pts',(95.2872935552373,-1.00388343251831,-6.04793535310837));
#22029=CARTESIAN_POINT('Ctrl Pts',(95.3262499490834,-1.0461209478446,-6.04497211414628));
#22030=CARTESIAN_POINT('Ctrl Pts',(95.365281100693,-1.08843951744378,-6.04200318869488));
#22031=CARTESIAN_POINT('Ctrl Pts',(95.40663721333,-1.12852024946172,-6.03903426324348));
#22032=CARTESIAN_POINT('Ctrl Pts',(95.4500223219213,-1.16611421473036,-6.03606533779207));
#22033=CARTESIAN_POINT('Ctrl Pts',(95.4887760484797,-1.19969500541112,-6.03341334661695));
#22034=CARTESIAN_POINT('Ctrl Pts',(95.529148010317,-1.23129202170489,-6.03076135544183));
#22035=CARTESIAN_POINT('Ctrl Pts',(95.5709078972908,-1.26075722668808,-6.0281093642667));
#22036=CARTESIAN_POINT('Ctrl Pts',(95.6176788115735,-1.29375814399077,-6.0251391442561));
#22037=CARTESIAN_POINT('Ctrl Pts',(95.666385876195,-1.32422155670154,-6.02216892424549));
#22038=CARTESIAN_POINT('Ctrl Pts',(95.7167228900047,-1.35191454937851,-6.01919870423488));
#22039=CARTESIAN_POINT('Ctrl Pts',(95.7669710054558,-1.37955863447417,-6.01623372982118));
#22040=CARTESIAN_POINT('Ctrl Pts',(95.8188429034369,-1.40444176173788,-6.01326875540748));
#22041=CARTESIAN_POINT('Ctrl Pts',(95.872003214868,-1.42637405884705,-6.01030378099378));
#22042=CARTESIAN_POINT('Ctrl Pts',(95.9251110704837,-1.44828471431229,-6.00734173226178));
#22043=CARTESIAN_POINT('Ctrl Pts',(95.9795043411007,-1.46725011089183,-6.00437968352979));
#22044=CARTESIAN_POINT('Ctrl Pts',(96.0348244283148,-1.48312694193954,-6.0014176347978));
#22045=CARTESIAN_POINT('Ctrl Pts',(96.090111223882,-1.49899421830504,-5.99845736862772));
#22046=CARTESIAN_POINT('Ctrl Pts',(96.1463232303117,-1.51177647021289,-5.99549710245764));
#22047=CARTESIAN_POINT('Ctrl Pts',(96.203085403343,-1.52137981213729,-5.99253683628756));
#22048=CARTESIAN_POINT('Ctrl Pts',(96.259835266122,-1.53098107134435,-5.98957721212291));
#22049=CARTESIAN_POINT('Ctrl Pts',(96.3171345448594,-1.53740470253106,-5.98661758795826));
#22050=CARTESIAN_POINT('Ctrl Pts',(96.3745988768833,-1.5406080843582,-5.98365796379361));
#22051=CARTESIAN_POINT('Ctrl Pts',(96.432115053852,-1.54381435631123,-5.98069566942388));
#22052=CARTESIAN_POINT('Ctrl Pts',(96.4897960600159,-1.54379454334605,-5.97773337505415));
#22053=CARTESIAN_POINT('Ctrl Pts',(96.5472546827378,-1.54055811939484,-5.97477108068442));
#22054=CARTESIAN_POINT('Ctrl Pts',(96.6047375755878,-1.53732032840034,-5.97180753506187));
#22055=CARTESIAN_POINT('Ctrl Pts',(96.661997378546,-1.53086327533476,-5.96884398943931));
#22056=CARTESIAN_POINT('Ctrl Pts',(96.7186524035503,-1.52124833618752,-5.96588044381675));
#22057=CARTESIAN_POINT('Ctrl Pts',(96.7754160898408,-1.51161495610494,-5.96291121427333));
#22058=CARTESIAN_POINT('Ctrl Pts',(96.8315721702688,-1.49881170294986,-5.95994198472991));
#22059=CARTESIAN_POINT('Ctrl Pts',(96.8867505062524,-1.48295086400454,-5.95697275518648));
#22060=CARTESIAN_POINT('Ctrl Pts',(96.9359885888775,-1.46879753218377,-5.95432317964228));
#22061=CARTESIAN_POINT('Ctrl Pts',(96.984448079226,-1.45221031159443,-5.95167360409808));
#22062=CARTESIAN_POINT('Ctrl Pts',(97.031879979471,-1.43330113675956,-5.94902402855388));
#22063=CARTESIAN_POINT('Ctrl Pts',(97.085052000573,-1.41210360855282,-5.94605380627688));
#22064=CARTESIAN_POINT('Ctrl Pts',(97.1371534399318,-1.3878991580331,-5.94308358399989));
#22065=CARTESIAN_POINT('Ctrl Pts',(97.1878220574034,-1.3608173694019,-5.94011336172289));
#22066=CARTESIAN_POINT('Ctrl Pts',(97.2384012160943,-1.33378339545187,-5.93714838356891));
#22067=CARTESIAN_POINT('Ctrl Pts',(97.2875521180855,-1.30388241050893,-5.93418340541494));
#22068=CARTESIAN_POINT('Ctrl Pts',(97.3349326881829,-1.27129192432311,-5.93121842726096));
#22069=CARTESIAN_POINT('Ctrl Pts',(97.3822665199763,-1.23873358684393,-5.92825637389345));
#22070=CARTESIAN_POINT('Ctrl Pts',(97.4278330525774,-1.20349129864964,-5.92529432052594));
#22071=CARTESIAN_POINT('Ctrl Pts',(97.4713165676437,-1.16578743913617,-5.92233226715843));
#22072=CARTESIAN_POINT('Ctrl Pts',(97.5147739273687,-1.12810625850026,-5.91937199546649));
#22073=CARTESIAN_POINT('Ctrl Pts',(97.5561503602495,-1.08796678250313,-5.91641172377456));
#22074=CARTESIAN_POINT('Ctrl Pts',(97.5951625982189,-1.0456321323655,-5.91345145208262));
#22075=CARTESIAN_POINT('Ctrl Pts',(97.6341663870328,-1.00330665094165,-5.91049182151761));
#22076=CARTESIAN_POINT('Ctrl Pts',(97.6708066445105,-0.95878732250894,-5.90753219095259));
#22077=CARTESIAN_POINT('Ctrl Pts',(97.7048379854176,-0.912373041772958,
-5.90457256038758));
#22078=CARTESIAN_POINT('Ctrl Pts',(97.7389000450271,-0.865916864760098,
-5.90161025828485));
#22079=CARTESIAN_POINT('Ctrl Pts',(97.7703481726039,-0.817562738317025,
-5.89864795618211));
#22080=CARTESIAN_POINT('Ctrl Pts',(97.7989790905744,-0.767640362765306,
-5.89568565407938));
#22081=CARTESIAN_POINT('Ctrl Pts',(97.8276221092052,-0.717696887865466,
-5.89272209998007));
#22082=CARTESIAN_POINT('Ctrl Pts',(97.8534453095478,-0.666184309021905,
-5.88975854588076));
#22083=CARTESIAN_POINT('Ctrl Pts',(97.8762919280009,-0.613456007692871,
-5.88679499178145));
#22084=CARTESIAN_POINT('Ctrl Pts',(97.8991823737796,-0.560626556145983,
-5.88382575261103));
#22085=CARTESIAN_POINT('Ctrl Pts',(97.9190846462876,-0.50657721251163,-5.88085651344061));
#22086=CARTESIAN_POINT('Ctrl Pts',(97.9358909518878,-0.45167944947849,-5.87788727427019));
#22087=CARTESIAN_POINT('Ctrl Pts',(97.9508876430623,-0.402692788283397,
-5.87523774712714));
#22088=CARTESIAN_POINT('Ctrl Pts',(97.9634198405777,-0.35303104463705,-5.8725882199841));
#22089=CARTESIAN_POINT('Ctrl Pts',(97.9734455377117,-0.302963950083964,
-5.86993869284106));
#22090=CARTESIAN_POINT('Ctrl Pts',(97.9895138161738,-0.222720949889708,
-5.86569227093558));
#22091=CARTESIAN_POINT('Ctrl Pts',(97.9992020858234,-0.141160850084212,
-5.8614458490301));
#22092=CARTESIAN_POINT('Ctrl Pts',(98.0023478318077,-0.0591229014857949,
-5.85719942712462));
#22093=CARTESIAN_POINT('Ctrl Pts',(98.0030855946121,-0.0398827761472533,
-5.85620352594598));
#22094=CARTESIAN_POINT('Ctrl Pts',(98.003463688527,-0.0206164838043829,
-5.85520762476735));
#22095=CARTESIAN_POINT('Ctrl Pts',(98.0034803719723,-0.00133509838387759,
-5.85421172358872));
#22096=CARTESIAN_POINT('Ctrl Pts',(98.0034803719729,-0.00133509777570635,
-5.85421172355731));
#22097=CARTESIAN_POINT('Ctrl Pts',(98.003529319685,0.0552347602601169,-5.85128983868941));
#22098=CARTESIAN_POINT('Ctrl Pts',(98.0004630541371,0.111904542497342,-5.84836795382152));
#22099=CARTESIAN_POINT('Ctrl Pts',(97.9942751962306,0.16829797661396,-5.84544606895362));
#22100=CARTESIAN_POINT('Ctrl Pts',(97.9880929098134,0.224640634610309,-5.84252681492351));
#22101=CARTESIAN_POINT('Ctrl Pts',(97.9787946528756,0.280706904815718,-5.8396075608934));
#22102=CARTESIAN_POINT('Ctrl Pts',(97.9664260609476,0.336122479966725,-5.83668830686329));
#22103=CARTESIAN_POINT('Ctrl Pts',(97.9540635171348,0.391510957467202,-5.8337704803186));
#22104=CARTESIAN_POINT('Ctrl Pts',(97.9386337296698,0.446248846150917,-5.83085265377392));
#22105=CARTESIAN_POINT('Ctrl Pts',(97.9202335485138,0.499971349076287,-5.82793482722923));
#22106=CARTESIAN_POINT('Ctrl Pts',(97.9018347962476,0.553689680111704,-5.82501722727211));
#22107=CARTESIAN_POINT('Ctrl Pts',(97.8804662849714,0.606392274179094,-5.82209962731498));
#22108=CARTESIAN_POINT('Ctrl Pts',(97.8562741596734,0.657731187225284,-5.81918202735786));
#22109=CARTESIAN_POINT('Ctrl Pts',(97.8320584704108,0.709120106143976,-5.81626158555772));
#22110=CARTESIAN_POINT('Ctrl Pts',(97.80501391234,0.759142208116028,-5.81334114375759));
#22111=CARTESIAN_POINT('Ctrl Pts',(97.7753333147438,0.807472759797698,-5.81042070195745));
#22112=CARTESIAN_POINT('Ctrl Pts',(97.7456350511605,0.855832077979083,-5.80749852190096));
#22113=CARTESIAN_POINT('Ctrl Pts',(97.7132979367514,0.902497403768863,-5.80457634184448));
#22114=CARTESIAN_POINT('Ctrl Pts',(97.6785570974921,0.947174481223082,-5.801654161788));
#22115=CARTESIAN_POINT('Ctrl Pts',(97.6437576822231,0.991926888029769,-5.7987270546874));
#22116=CARTESIAN_POINT('Ctrl Pts',(97.6065468178134,1.0346839619332,-5.7957999475868));
#22117=CARTESIAN_POINT('Ctrl Pts',(97.5671975262562,1.07518715529138,-5.7928728404862));
#22118=CARTESIAN_POINT('Ctrl Pts',(97.558148177449,1.08450187253272,-5.79219967936688));
#22119=CARTESIAN_POINT('Ctrl Pts',(97.548985869182,1.09369755351201,-5.79152651824756));
#22120=CARTESIAN_POINT('Ctrl Pts',(97.539714160954,1.10277136137139,-5.79085335712823));
#22121=CARTESIAN_POINT('Ctrl Pts',(97.4988040775081,1.14280823780976,-5.78788313018766));
#22122=CARTESIAN_POINT('Ctrl Pts',(97.4555779765147,1.18064881807926,-5.78491290324709));
#22123=CARTESIAN_POINT('Ctrl Pts',(97.4103009999711,1.21601433867756,-5.78194267630652));
#22124=CARTESIAN_POINT('Ctrl Pts',(97.3651039890387,1.25131739871226,-5.77897769521121));
#22125=CARTESIAN_POINT('Ctrl Pts',(97.3178636995138,1.28415375726168,-5.7760127141159));
#22126=CARTESIAN_POINT('Ctrl Pts',(97.2688809318777,1.31428249193853,-5.77304773302059));
#22127=CARTESIAN_POINT('Ctrl Pts',(97.2199465003075,1.34438149565954,-5.7700856777608));
#22128=CARTESIAN_POINT('Ctrl Pts',(97.1692734392942,1.37177789762699,-5.76712362250101));
#22129=CARTESIAN_POINT('Ctrl Pts',(97.1171929069576,1.39627304100358,-5.76416156724122));
#22130=CARTESIAN_POINT('Ctrl Pts',(97.0651437194437,1.42075344190551,-5.76120129470317));
#22131=CARTESIAN_POINT('Ctrl Pts',(97.0116892106127,1.44233582423702,-5.75824102216512));
#22132=CARTESIAN_POINT('Ctrl Pts',(96.9571846549207,1.4608676973285,-5.75528074962707));
#22133=CARTESIAN_POINT('Ctrl Pts',(96.9026919228934,1.47939555030363,-5.75232111926048));
#22134=CARTESIAN_POINT('Ctrl Pts',(96.847150089584,1.49487404023915,-5.74936148889388));
#22135=CARTESIAN_POINT('Ctrl Pts',(96.7909318034718,1.50719979868635,-5.74640185852729));
#22136=CARTESIAN_POINT('Ctrl Pts',(96.7346628023357,1.51953667631163,-5.7434395582514));
#22137=CARTESIAN_POINT('Ctrl Pts',(96.677716639199,1.52871502645337,-5.74047725797551));
#22138=CARTESIAN_POINT('Ctrl Pts',(96.6204770833966,1.53468245482991,-5.73751495769962));
#22139=CARTESIAN_POINT('Ctrl Pts',(96.5632133529976,1.5406524034946,-5.73455140632363));
#22140=CARTESIAN_POINT('Ctrl Pts',(96.5056565046217,1.5434087009063,-5.73158785494763));
#22141=CARTESIAN_POINT('Ctrl Pts',(96.4481931303532,1.54295107164768,-5.72862430357164));
#22142=CARTESIAN_POINT('Ctrl Pts',(96.3906195508084,1.5424925647316,-5.72565506859278));
#22143=CARTESIAN_POINT('Ctrl Pts',(96.333140325593,1.53880784726999,-5.72268583361393));
#22144=CARTESIAN_POINT('Ctrl Pts',(96.2761387637044,1.53194874539186,-5.71971659863507));
#22145=CARTESIAN_POINT('Ctrl Pts',(96.2252747847625,1.52582819006092,-5.71706707289519));
#22146=CARTESIAN_POINT('Ctrl Pts',(96.1747913058088,1.51718083018387,-5.7144175471553));
#22147=CARTESIAN_POINT('Ctrl Pts',(96.1249519726324,1.5060774567168,-5.71176802141541));
#22148=CARTESIAN_POINT('Ctrl Pts',(96.0690995587969,1.4936344690135,-5.70879883224972));
#22149=CARTESIAN_POINT('Ctrl Pts',(96.0138241261216,1.47805450256403,-5.70582964308403));
#22150=CARTESIAN_POINT('Ctrl Pts',(95.9595035514066,1.45940763548859,-5.70286045391834));
#22151=CARTESIAN_POINT('Ctrl Pts',(95.9052573561847,1.44078630099503,-5.6998953303721));
#22152=CARTESIAN_POINT('Ctrl Pts',(95.8519639179068,1.41910655099664,-5.69693020682586));
#22153=CARTESIAN_POINT('Ctrl Pts',(95.7999893008411,1.39448907559369,-5.69396508327963));
#22154=CARTESIAN_POINT('Ctrl Pts',(95.7480668880911,1.36989632646156,-5.69100293796112));
#22155=CARTESIAN_POINT('Ctrl Pts',(95.6974611404136,1.34237192135134,-5.68804079264261));
#22156=CARTESIAN_POINT('Ctrl Pts',(95.6485192377665,1.31208505004585,-5.6850786473241));
#22157=CARTESIAN_POINT('Ctrl Pts',(95.6044256191205,1.2847984575536,-5.68240993812024));
#22158=CARTESIAN_POINT('Ctrl Pts',(95.5616825337404,1.25527035238062,-5.67974122891638));
#22159=CARTESIAN_POINT('Ctrl Pts',(95.5205266553345,1.22365637526844,-5.67707251971253));
#22160=CARTESIAN_POINT('',(98.0034806047664,0.00103154524370014,-5.89578827637723));
#22161=CARTESIAN_POINT('Ctrl Pts',(98.0034806047663,0.00103154524370189,
-5.89578827637723));
#22162=CARTESIAN_POINT('Ctrl Pts',(98.0034368144072,0.0665337706066547,
-5.89242239470813));
#22163=CARTESIAN_POINT('Ctrl Pts',(97.9992179907216,0.131874306095174,-5.88905651303903));
#22164=CARTESIAN_POINT('Ctrl Pts',(97.9909097815011,0.196561925141776,-5.88569063136993));
#22165=CARTESIAN_POINT('Ctrl Pts',(97.9825300313629,0.261806560930387,-5.88229576652803));
#22166=CARTESIAN_POINT('Ctrl Pts',(97.9699902874583,0.326386762739351,-5.87890090168612));
#22167=CARTESIAN_POINT('Ctrl Pts',(97.9534281470382,0.389817477279625,-5.87550603684422));
#22168=CARTESIAN_POINT('Ctrl Pts',(97.9401116843809,0.440817693439974,-5.87277646266194));
#22169=CARTESIAN_POINT('Ctrl Pts',(97.9241958691204,0.49107513427045,-5.87004688847967));
#22170=CARTESIAN_POINT('Ctrl Pts',(97.9057744059364,0.540347874063355,-5.86731731429739));
#22171=CARTESIAN_POINT('Ctrl Pts',(97.8857288623146,0.593964616936417,-5.86434709429949));
#22172=CARTESIAN_POINT('Ctrl Pts',(97.8626540129301,0.646575917569546,-5.8613768743016));
#22173=CARTESIAN_POINT('Ctrl Pts',(97.836671590467,0.697816824049706,-5.8584066543037));
#22174=CARTESIAN_POINT('Ctrl Pts',(97.8107350546114,0.748967235836129,-5.85544167990288));
#22175=CARTESIAN_POINT('Ctrl Pts',(97.7819013717319,0.798751596087378,-5.85247670550206));
#22176=CARTESIAN_POINT('Ctrl Pts',(97.7503406242082,0.846824078401311,-5.84951173110124));
#22177=CARTESIAN_POINT('Ctrl Pts',(97.718811019181,0.894849125301756,-5.84654968238222));
#22178=CARTESIAN_POINT('Ctrl Pts',(97.6845599658042,0.941165207505367,-5.8435876336632));
#22179=CARTESIAN_POINT('Ctrl Pts',(97.6478029747452,0.985451880383085,-5.84062558494418));
#22180=CARTESIAN_POINT('Ctrl Pts',(97.6110681040566,1.0297119015252,-5.83766531878714));
#22181=CARTESIAN_POINT('Ctrl Pts',(97.5718306174779,1.07194453405626,-5.8347050526301));
#22182=CARTESIAN_POINT('Ctrl Pts',(97.5303474586884,1.11186089628237,-5.83174478647306));
#22183=CARTESIAN_POINT('Ctrl Pts',(97.4888732965275,1.15176860167767,-5.82878516232149));
#22184=CARTESIAN_POINT('Ctrl Pts',(97.4451548046207,1.18936067291497,-5.82582553816993));
#22185=CARTESIAN_POINT('Ctrl Pts',(97.3994855097825,1.22438532983422,-5.82286591401837));
#22186=CARTESIAN_POINT('Ctrl Pts',(97.3537750116096,1.25944158638005,-5.8199036196617));
#22187=CARTESIAN_POINT('Ctrl Pts',(97.3061106076032,1.29192548128931,-5.81694132530502));
#22188=CARTESIAN_POINT('Ctrl Pts',(97.2568175320717,1.32162666717219,-5.81397903094835));
#22189=CARTESIAN_POINT('Ctrl Pts',(97.2075036354831,1.35134039863232,-5.81101548533885));
#22190=CARTESIAN_POINT('Ctrl Pts',(97.1565601572544,1.37826883282067,-5.80805193972935));
#22191=CARTESIAN_POINT('Ctrl Pts',(97.1043370116834,1.40224761411417,-5.80508839411985));
#22192=CARTESIAN_POINT('Ctrl Pts',(97.0520137049289,1.42627238542005,-5.80211916458932));
#22193=CARTESIAN_POINT('Ctrl Pts',(96.9984063130631,1.44733600738197,-5.79914993505879));
#22194=CARTESIAN_POINT('Ctrl Pts',(96.9438838946454,1.4653226923443,-5.79618070552826));
#22195=CARTESIAN_POINT('Ctrl Pts',(96.8952311143135,1.48137301178664,-5.79353112988036));
#22196=CARTESIAN_POINT('Ctrl Pts',(96.8458501985461,1.49497387408799,-5.79088155423246));
#22197=CARTESIAN_POINT('Ctrl Pts',(96.7960099265794,1.50607745670391,-5.78823197858457));
#22198=CARTESIAN_POINT('Ctrl Pts',(96.7401574615112,1.51852045582324,-5.78526278669454));
#22199=CARTESIAN_POINT('Ctrl Pts',(96.6834957764216,1.52787820917547,-5.78229359480452));
#22200=CARTESIAN_POINT('Ctrl Pts',(96.6263967605175,1.53405376166546,-5.7793244029145));
#22201=CARTESIAN_POINT('Ctrl Pts',(96.569378102475,1.54022062303907,-5.77635938969389));
#22202=CARTESIAN_POINT('Ctrl Pts',(96.5119238464598,1.54321410043556,-5.77339437647328));
#22203=CARTESIAN_POINT('Ctrl Pts',(96.4544166265746,1.54298808290489,-5.77042936325266));
#22204=CARTESIAN_POINT('Ctrl Pts',(96.3969681978041,1.54276229643778,-5.76746738124157));
#22205=CARTESIAN_POINT('Ctrl Pts',(96.3394674311735,1.53932354061843,-5.76450539923047));
#22206=CARTESIAN_POINT('Ctrl Pts',(96.2823004289469,1.53267762496487,-5.76154341721937));
#22207=CARTESIAN_POINT('Ctrl Pts',(96.2251698629896,1.52603594518802,-5.75858332307313));
#22208=CARTESIAN_POINT('Ctrl Pts',(96.1683731561569,1.51619122001913,-5.75562322892688));
#22209=CARTESIAN_POINT('Ctrl Pts',(96.1122925199385,1.50320118994959,-5.75266313478064));
#22210=CARTESIAN_POINT('Ctrl Pts',(96.0561991149433,1.49020820223183,-5.74970236666235));
#22211=CARTESIAN_POINT('Ctrl Pts',(96.0008226179281,1.47406858140213,-5.74674159854406));
#22212=CARTESIAN_POINT('Ctrl Pts',(95.946534597265,1.45489111171426,-5.74378083042577));
#22213=CARTESIAN_POINT('Ctrl Pts',(95.8922431486712,1.4357124310956,-5.74081987535449));
#22214=CARTESIAN_POINT('Ctrl Pts',(95.8390408011915,1.41349570508005,-5.73785892028321));
#22215=CARTESIAN_POINT('Ctrl Pts',(95.7872807856092,1.3883985520137,-5.73489796521193));
#22216=CARTESIAN_POINT('Ctrl Pts',(95.7354547427195,1.36326938393691,-5.73193323301871));
#22217=CARTESIAN_POINT('Ctrl Pts',(95.6850751706515,1.33525269038501,-5.72896850082549));
#22218=CARTESIAN_POINT('Ctrl Pts',(95.6364710924078,1.30455231987372,-5.72600376863226));
#22219=CARTESIAN_POINT('Ctrl Pts',(95.5965714697968,1.27935004793117,-5.72356998735451));
#22220=CARTESIAN_POINT('Ctrl Pts',(95.5578679692882,1.25234018643704,-5.72113620607676));
#22221=CARTESIAN_POINT('Ctrl Pts',(95.5205266553345,1.22365637526844,-5.71870242479901));
#22222=CARTESIAN_POINT('Ctrl Pts',(95.5205266553345,1.22365637526844,-6.21868058178697));
#22223=CARTESIAN_POINT('Ctrl Pts',(95.4747790085359,1.18851522132283,-6.2157136542204));
#22224=CARTESIAN_POINT('Ctrl Pts',(95.4310162232319,1.15081399765501,-6.21274672665382));
#22225=CARTESIAN_POINT('Ctrl Pts',(95.3895264706737,1.11081299241457,-6.20977979908725));
#22226=CARTESIAN_POINT('Ctrl Pts',(95.348019423428,1.07079531305955,-6.20681163477949));
#22227=CARTESIAN_POINT('Ctrl Pts',(95.3087876529973,1.02847632164036,-6.20384347047174));
#22228=CARTESIAN_POINT('Ctrl Pts',(95.2720813174728,0.984152078905769,-6.20087530616399));
#22229=CARTESIAN_POINT('Ctrl Pts',(95.2353040281644,0.93974215688186,-6.19790140435927));
#22230=CARTESIAN_POINT('Ctrl Pts',(95.201062239961,0.893319656152468,-6.19492750255455));
#22231=CARTESIAN_POINT('Ctrl Pts',(95.1695642023373,0.845211779198604,-6.19195360074983));
#22232=CARTESIAN_POINT('Ctrl Pts',(95.1402789442497,0.800483545348947,-6.18918861954945));
#22233=CARTESIAN_POINT('Ctrl Pts',(95.113365174356,0.754299010827867,-6.18642363834907));
#22234=CARTESIAN_POINT('Ctrl Pts',(95.0889538337176,0.70693873175991,-6.18365865714869));
#22235=CARTESIAN_POINT('Ctrl Pts',(95.0627503898425,0.656101605161792,-6.18069069112123));
#22236=CARTESIAN_POINT('Ctrl Pts',(95.0393219794477,0.6036983292004,-6.17772272509376));
#22237=CARTESIAN_POINT('Ctrl Pts',(95.0188572007958,0.550063602640737,-6.1747547590663));
#22238=CARTESIAN_POINT('Ctrl Pts',(94.9984289007308,0.496524480292817,-6.17179208345552));
#22239=CARTESIAN_POINT('Ctrl Pts',(94.9809539321004,0.441758747919574,-6.16882940784474));
#22240=CARTESIAN_POINT('Ctrl Pts',(94.9665742703897,0.386124117195004,-6.16586673223397));
#22241=CARTESIAN_POINT('Ctrl Pts',(94.9522089333496,0.330544908341546,-6.16290700796885));
#22242=CARTESIAN_POINT('Ctrl Pts',(94.9409329242954,0.274099019051727,-6.15994728370373));
#22243=CARTESIAN_POINT('Ctrl Pts',(94.9328389151162,0.217160803434828,-6.15698755943861));
#22244=CARTESIAN_POINT('Ctrl Pts',(94.9247498396805,0.160257294790163,-6.15402963928812));
#22245=CARTESIAN_POINT('Ctrl Pts',(94.9198389927644,0.102862570642138,-6.15107171913764));
#22246=CARTESIAN_POINT('Ctrl Pts',(94.9181478388104,0.0453605052125778,
-6.14811379898715));
#22247=CARTESIAN_POINT('Ctrl Pts',(94.916457061906,-0.0121287399019599,
-6.14515653831677));
#22248=CARTESIAN_POINT('Ctrl Pts',(94.9179845681433,-0.0697247570523037,
-6.14219927764639));
#22249=CARTESIAN_POINT('Ctrl Pts',(94.9227197642528,-0.127041477126066,
-6.13924201697601));
#22250=CARTESIAN_POINT('Ctrl Pts',(94.9274592224977,-0.184409787801061,
-6.13628209448451));
#22251=CARTESIAN_POINT('Ctrl Pts',(94.935412097954,-0.241497777290012,-6.133322171993));
#22252=CARTESIAN_POINT('Ctrl Pts',(94.946515804449,-0.297923713956436,-6.1303622495015));
#22253=CARTESIAN_POINT('Ctrl Pts',(94.9576241731273,-0.354373342536782,
-6.12740108420868));
#22254=CARTESIAN_POINT('Ctrl Pts',(94.9718858815279,-0.410159856896842,
-6.12443991891585));
#22255=CARTESIAN_POINT('Ctrl Pts',(94.9891876960229,-0.464914144811771,
-6.12147875362302));
#22256=CARTESIAN_POINT('Ctrl Pts',(95.0065228181682,-0.519773839976079,
-6.11851188780335));
#22257=CARTESIAN_POINT('Ctrl Pts',(95.0269095559865,-0.573596847731523,
-6.11554502198367));
#22258=CARTESIAN_POINT('Ctrl Pts',(95.050185840517,-0.626032511425179,-6.11257815616399));
#22259=CARTESIAN_POINT('Ctrl Pts',(95.0711195825055,-0.673191011026923,
-6.10990987792128));
#22260=CARTESIAN_POINT('Ctrl Pts',(95.0943897497026,-0.719227411779942,
-6.10724159967858));
#22261=CARTESIAN_POINT('Ctrl Pts',(95.1198477222013,-0.763905458585111,
-6.10457332143587));
#22262=CARTESIAN_POINT('Ctrl Pts',(95.1481877206498,-0.813641382261066,
-6.10160297486713));
#22263=CARTESIAN_POINT('Ctrl Pts',(95.1793581390997,-0.86190156408254,-6.0986326282984));
#22264=CARTESIAN_POINT('Ctrl Pts',(95.2131805995963,-0.908345108941542,
-6.09566228172966));
#22265=CARTESIAN_POINT('Ctrl Pts',(95.2469432703009,-0.95470655303541,-6.09269718600315));
#22266=CARTESIAN_POINT('Ctrl Pts',(95.2833483732805,-0.999257316401485,
-6.08973209027663));
#22267=CARTESIAN_POINT('Ctrl Pts',(95.3221728492778,-1.04168309422453,-6.08676699455011));
#22268=CARTESIAN_POINT('Ctrl Pts',(95.360958973831,-1.08406696317938,-6.08380482779301));
#22269=CARTESIAN_POINT('Ctrl Pts',(95.4021593860605,-1.12432962298756,-6.08084266103592));
#22270=CARTESIAN_POINT('Ctrl Pts',(95.445510226097,-1.16218906830109,-6.07788049427882));
#22271=CARTESIAN_POINT('Ctrl Pts',(95.4888349273732,-1.20002568593778,-6.07492011358554));
#22272=CARTESIAN_POINT('Ctrl Pts',(95.5343070942845,-1.23546161940882,-6.07195973289227));
#22273=CARTESIAN_POINT('Ctrl Pts',(95.5816269954335,-1.26825262754952,-6.06899935219899));
#22274=CARTESIAN_POINT('Ctrl Pts',(95.6289365750507,-1.30103648323592,-6.06603961723114));
#22275=CARTESIAN_POINT('Ctrl Pts',(95.6780926604554,-1.33117626234097,-6.06307988226328));
#22276=CARTESIAN_POINT('Ctrl Pts',(95.7287653189123,-1.35847018216852,-6.06012014729543));
#22277=CARTESIAN_POINT('Ctrl Pts',(95.7794835769142,-1.38578866337424,-6.05715774890766));
#22278=CARTESIAN_POINT('Ctrl Pts',(95.8317206755153,-1.41025591932714,-6.05419535051988));
#22279=CARTESIAN_POINT('Ctrl Pts',(95.8851219847079,-1.43171612463671,-6.0512329521321));
#22280=CARTESIAN_POINT('Ctrl Pts',(95.9385457853317,-1.45318536850242,-6.04826930604871));
#22281=CARTESIAN_POINT('Ctrl Pts',(95.9931342796287,-1.47164486852846,-6.04530565996532));
#22282=CARTESIAN_POINT('Ctrl Pts',(96.0485158027972,-1.48698813641492,-6.04234201388192));
#22283=CARTESIAN_POINT('Ctrl Pts',(96.1040034037539,-1.50236079280185,-6.03937269122982));
#22284=CARTESIAN_POINT('Ctrl Pts',(96.1602865579545,-1.51460517806133,-6.03640336857772));
#22285=CARTESIAN_POINT('Ctrl Pts',(96.2169824419505,-1.52366580219669,-6.03343404592562));
#22286=CARTESIAN_POINT('Ctrl Pts',(96.2675561428979,-1.53174803432927,-6.03078535919143));
#22287=CARTESIAN_POINT('Ctrl Pts',(96.3184578788774,-1.5372976770742,-6.02813667245723));
#22288=CARTESIAN_POINT('Ctrl Pts',(96.369414962073,-1.54031035376639,-6.02548798572304));
#22289=CARTESIAN_POINT('Ctrl Pts',(96.4265650355648,-1.54368917146097,-6.02251739494305));
#22290=CARTESIAN_POINT('Ctrl Pts',(96.4840219219422,-1.54389003411547,-6.01954680416306));
#22291=CARTESIAN_POINT('Ctrl Pts',(96.5414025287611,-1.5408766005175,-6.01657621338308));
#22292=CARTESIAN_POINT('Ctrl Pts',(96.5986820643019,-1.53786847483804,-6.01361085505745));
#22293=CARTESIAN_POINT('Ctrl Pts',(96.6558850707543,-1.53165731786393,-6.01064549673183));
#22294=CARTESIAN_POINT('Ctrl Pts',(96.712626384826,-1.52225874262003,-6.00768013840621));
#22295=CARTESIAN_POINT('Ctrl Pts',(96.7693118646023,-1.51286941571369,-6.0047176980372));
#22296=CARTESIAN_POINT('Ctrl Pts',(96.8255360405538,-1.50029896973757,-6.00175525766819));
#22297=CARTESIAN_POINT('Ctrl Pts',(96.8809185815599,-1.48461483139992,-5.99879281729918));
#22298=CARTESIAN_POINT('Ctrl Pts',(96.9362679290057,-1.46894009336032,-5.99583215247064));
#22299=CARTESIAN_POINT('Ctrl Pts',(96.9907761410612,-1.45015550416919,-5.9928714876421));
#22300=CARTESIAN_POINT('Ctrl Pts',(97.0440749858331,-1.42837915164229,-5.98991082281356));
#22301=CARTESIAN_POINT('Ctrl Pts',(97.0973623869221,-1.40660747467026,-5.98695079366315));
#22302=CARTESIAN_POINT('Ctrl Pts',(97.149440454119,-1.3818455068257,-5.98399076451273));
#22303=CARTESIAN_POINT('Ctrl Pts',(97.1999600800918,-1.35425980355805,-5.98103073536232));
#22304=CARTESIAN_POINT('Ctrl Pts',(97.2505253930866,-1.32664915337898,-5.97806802933307));
#22305=CARTESIAN_POINT('Ctrl Pts',(97.299528989743,-1.29620991462818,-5.97510532330383));
#22306=CARTESIAN_POINT('Ctrl Pts',(97.3466468187319,-1.26315440558351,-5.97214261727459));
#22307=CARTESIAN_POINT('Ctrl Pts',(97.3937846159362,-1.23008488783888,-5.96917865567068));
#22308=CARTESIAN_POINT('Ctrl Pts',(97.4390346416185,-1.19439721201901,-5.96621469406677));
#22309=CARTESIAN_POINT('Ctrl Pts',(97.4821049123582,-1.15634487877593,-5.96325073246286));
#22310=CARTESIAN_POINT('Ctrl Pts',(97.5252578058132,-1.11821954884524,-5.96028108502155));
#22311=CARTESIAN_POINT('Ctrl Pts',(97.5662222164714,-1.0777208642979,-5.95731143758024));
#22312=CARTESIAN_POINT('Ctrl Pts',(97.6047428238428,-1.0351394896833,-5.95434179013894));
#22313=CARTESIAN_POINT('Ctrl Pts',(97.6390701871419,-0.99719340274645,-5.95169541009603));
#22314=CARTESIAN_POINT('Ctrl Pts',(97.6714572375037,-0.957594078838122,
-5.94904903005312));
#22315=CARTESIAN_POINT('Ctrl Pts',(97.7017520058931,-0.916567054149245,
-5.94640265001022));
#22316=CARTESIAN_POINT('Ctrl Pts',(97.7359095435129,-0.870308831566921,
-5.94341884024116));
#22317=CARTESIAN_POINT('Ctrl Pts',(97.7675493401887,-0.822041711790214,
-5.94043503047209));
#22318=CARTESIAN_POINT('Ctrl Pts',(97.7964295587994,-0.77206885283428,-5.93745122070303));
#22319=CARTESIAN_POINT('Ctrl Pts',(97.8252637154166,-0.722175697205116,
-5.93447216990854));
#22320=CARTESIAN_POINT('Ctrl Pts',(97.8513467650861,-0.670582637972176,
-5.93149311911405));
#22321=CARTESIAN_POINT('Ctrl Pts',(97.8744789895756,-0.61762330176256,-5.92851406831956));
#22322=CARTESIAN_POINT('Ctrl Pts',(97.8975810174734,-0.564733098180144,
-5.9255389063504));
#22323=CARTESIAN_POINT('Ctrl Pts',(97.9177396604431,-0.510480626667888,
-5.92256374438124));
#22324=CARTESIAN_POINT('Ctrl Pts',(97.9348012475247,-0.455223746150777,
-5.91958858241208));
#22325=CARTESIAN_POINT('Ctrl Pts',(97.9518495970124,-0.400009737855236,
-5.91661572878537));
#22326=CARTESIAN_POINT('Ctrl Pts',(97.9658055059916,-0.343793356931493,
-5.91364287515866));
#22327=CARTESIAN_POINT('Ctrl Pts',(97.9765642485778,-0.286950223019388,
-5.91067002153195));
#22328=CARTESIAN_POINT('Ctrl Pts',(97.9873211159564,-0.230116996647804,
-5.90769768606224));
#22329=CARTESIAN_POINT('Ctrl Pts',(97.9948818164853,-0.172657737517019,
-5.90472535059254));
#22330=CARTESIAN_POINT('Ctrl Pts',(97.9991925548639,-0.114959104708224,
-5.90175301512283));
#22331=CARTESIAN_POINT('Ctrl Pts',(98.0020760817902,-0.076363498410695,
-5.89976476888564));
#22332=CARTESIAN_POINT('Ctrl Pts',(98.0035064719747,-0.037661007893966,
-5.89777652264845));
#22333=CARTESIAN_POINT('Ctrl Pts',(98.0034806047668,0.00103154458141929,
-5.89578827641126));
#22334=CARTESIAN_POINT('Ctrl Pts',(95.5043589656634,0.823943515129422,-6.49867147181494));
#22335=CARTESIAN_POINT('Ctrl Pts',(95.2313273711832,0.507125615617518,-6.47230253119553));
#22336=CARTESIAN_POINT('Ctrl Pts',(95.0301651886135,-0.41430205054822,-6.41957181200518));
#22337=CARTESIAN_POINT('Ctrl Pts',(96.0282541226869,-1.42674737697425,-6.34047931424389));
#22338=CARTESIAN_POINT('Ctrl Pts',(97.4200723870437,-1.13963437637263,-6.26139397853106));
#22339=CARTESIAN_POINT('Ctrl Pts',(97.9392541762185,0.182147029996038,-6.18230864281824));
#22340=CARTESIAN_POINT('Ctrl Pts',(97.1144000113395,1.33894478249095,-6.10322330710542));
#22341=CARTESIAN_POINT('Ctrl Pts',(95.6950438149812,1.27835036330238,-6.02413797139259));
#22342=CARTESIAN_POINT('Ctrl Pts',(94.9715162077941,0.0558575875799088,
-5.94505263567977));
#22343=CARTESIAN_POINT('Ctrl Pts',(95.6014510801772,-1.21747314835048,-5.86596729996694));
#22344=CARTESIAN_POINT('Ctrl Pts',(97.0122595444212,-1.38408065930718,-5.78688196425412));
#22345=CARTESIAN_POINT('Ctrl Pts',(97.9214937080554,-0.292562534091784,
-5.70779662854129));
#22346=CARTESIAN_POINT('Ctrl Pts',(97.5026547470092,1.064906048784,-5.62871129282847));
#22347=CARTESIAN_POINT('Ctrl Pts',(96.1364757169747,1.45435879288526,-5.54962595711564));
#22348=CARTESIAN_POINT('Ctrl Pts',(95.064809124152,0.521798178599738,-5.47054062140283));
#22349=CARTESIAN_POINT('Ctrl Pts',(95.2618435898322,-0.885101436100427,
-5.39145528569));
#22350=CARTESIAN_POINT('Ctrl Pts',(96.548398339734,-1.48739510247996,-5.31236994997717));
#22351=CARTESIAN_POINT('Ctrl Pts',(97.7551431885111,-0.737721463002487,
-5.23328461426435));
#22352=CARTESIAN_POINT('Ctrl Pts',(97.7848018665854,0.682731210024832,-5.15419927855152));
#22353=CARTESIAN_POINT('Ctrl Pts',(96.6111236810192,1.48219061059408,-5.0751139428387));
#22354=CARTESIAN_POINT('Ctrl Pts',(95.2994978278247,0.93517180164541,-4.99602860712587));
#22355=CARTESIAN_POINT('Ctrl Pts',(95.0454088976356,-0.463506086877637,
-4.91694327141305));
#22356=CARTESIAN_POINT('Ctrl Pts',(95.7305669616929,-1.1113509684898,-4.86421971427117));
#22357=CARTESIAN_POINT('Ctrl Pts',(96.1344998019829,-1.21933935595969,-4.83785793570023));
#22358=CARTESIAN_POINT('Ctrl Pts',(95.4329527647036,0.885478211758894,-6.55309378487631));
#22359=CARTESIAN_POINT('Ctrl Pts',(95.1395303108646,0.544999353728263,-6.5267248442569));
#22360=CARTESIAN_POINT('Ctrl Pts',(94.9233447029623,-0.445243432481966,
-6.47399412506655));
#22361=CARTESIAN_POINT('Ctrl Pts',(95.9959740620038,-1.53330136447085,-6.39490162730526));
#22362=CARTESIAN_POINT('Ctrl Pts',(97.4917376977215,-1.22474586075344,-6.31581629159243));
#22363=CARTESIAN_POINT('Ctrl Pts',(98.049693618018,0.195750343848208,-6.23673095587962));
#22364=CARTESIAN_POINT('Ctrl Pts',(97.1632367463181,1.43894139570691,-6.15764562016679));
#22365=CARTESIAN_POINT('Ctrl Pts',(95.6378785591096,1.37382159445786,-6.07856028445398));
#22366=CARTESIAN_POINT('Ctrl Pts',(94.8603156315467,0.060029208137714,-5.99947494874113));
#22367=CARTESIAN_POINT('Ctrl Pts',(95.5372960241103,-1.30839787736726,-5.92038961302833));
#22368=CARTESIAN_POINT('Ctrl Pts',(97.0534681076501,-1.48744816195426,-5.84130427731549));
#22369=CARTESIAN_POINT('Ctrl Pts',(98.0306067421578,-0.314412025531326,
-5.76221894160267));
#22370=CARTESIAN_POINT('Ctrl Pts',(97.5804875684133,1.14443658631183,-5.68313360588984));
#22371=CARTESIAN_POINT('Ctrl Pts',(96.1122779857853,1.56297488788122,-5.60404827017702));
#22372=CARTESIAN_POINT('Ctrl Pts',(94.9605759567141,0.56076770992362,-5.52496293446419));
#22373=CARTESIAN_POINT('Ctrl Pts',(95.1723255768299,-0.951203598878167,
-5.44587759875138));
#22374=CARTESIAN_POINT('Ctrl Pts',(96.5549642873171,-1.59847845312067,-5.36679226303854));
#22375=CARTESIAN_POINT('Ctrl Pts',(97.8518326419112,-0.792816825232235,
-5.28770692732572));
#22376=CARTESIAN_POINT('Ctrl Pts',(97.8837063234708,0.733719726976447,-5.20862159161289));
#22377=CARTESIAN_POINT('Ctrl Pts',(96.622374154636,1.59288527338979,-5.12953625590007));
#22378=CARTESIAN_POINT('Ctrl Pts',(95.2127919519034,1.00501337701317,-5.05045092018725));
#22379=CARTESIAN_POINT('Ctrl Pts',(94.9397268601826,-0.498122181207173,
-4.97136558447442));
#22380=CARTESIAN_POINT('Ctrl Pts',(95.6760546862938,-1.19435015889442,-4.91864202733255));
#22381=CARTESIAN_POINT('Ctrl Pts',(96.1101545032388,-1.31040345923813,-4.89228024876161));
#22382=CARTESIAN_POINT('Ctrl Pts',(95.3615465637438,0.947012908388365,-6.60751609793768));
#22383=CARTESIAN_POINT('Ctrl Pts',(95.0477332505459,0.582873091839006,-6.58114715731827));
#22384=CARTESIAN_POINT('Ctrl Pts',(94.8165242173111,-0.476184814415712,
-6.52841643812792));
#22385=CARTESIAN_POINT('Ctrl Pts',(95.9636940013207,-1.63985535196744,-6.44932394036664));
#22386=CARTESIAN_POINT('Ctrl Pts',(97.5634030083993,-1.30985734513425,-6.37023860465382));
#22387=CARTESIAN_POINT('Ctrl Pts',(98.1601330598174,0.209353657700377,-6.29115326894099));
#22388=CARTESIAN_POINT('Ctrl Pts',(97.2120734812969,1.53893800892286,-6.21206793322817));
#22389=CARTESIAN_POINT('Ctrl Pts',(95.5807133032378,1.46929282561336,-6.13298259751535));
#22390=CARTESIAN_POINT('Ctrl Pts',(94.7491150552996,0.0642008286955192,
-6.05389726180251));
#22391=CARTESIAN_POINT('Ctrl Pts',(95.4731409680433,-1.39932260638405,-5.9748119260897));
#22392=CARTESIAN_POINT('Ctrl Pts',(97.0946766708791,-1.59081566460134,-5.89572659037687));
#22393=CARTESIAN_POINT('Ctrl Pts',(98.1397197762602,-0.33626151697087,-5.81664125466405));
#22394=CARTESIAN_POINT('Ctrl Pts',(97.6583203898173,1.22396712383966,-5.73755591895122));
#22395=CARTESIAN_POINT('Ctrl Pts',(96.0880802545957,1.67159098287717,-5.6584705832384));
#22396=CARTESIAN_POINT('Ctrl Pts',(94.8563427892762,0.599737241247502,-5.57938524752557));
#22397=CARTESIAN_POINT('Ctrl Pts',(95.0828075638274,-1.01730576165591,-5.50029991181274));
#22398=CARTESIAN_POINT('Ctrl Pts',(96.5615302349002,-1.7095618037614,-5.42121457609992));
#22399=CARTESIAN_POINT('Ctrl Pts',(97.9485220953112,-0.847912187461983,
-5.3421292403871));
#22400=CARTESIAN_POINT('Ctrl Pts',(97.9826107803565,0.784708243928062,-5.26304390467428));
#22401=CARTESIAN_POINT('Ctrl Pts',(96.6336246282528,1.70357993618549,-5.18395856896145));
#22402=CARTESIAN_POINT('Ctrl Pts',(95.1260860759822,1.07485495238092,-5.10487323324863));
#22403=CARTESIAN_POINT('Ctrl Pts',(94.8340448227295,-0.532738275536707,
-5.0257878975358));
#22404=CARTESIAN_POINT('Ctrl Pts',(95.6215424108947,-1.27734934929906,-4.97306434039392));
#22405=CARTESIAN_POINT('Ctrl Pts',(96.0858092044945,-1.40146756251658,-4.94670256182298));
#22406=CARTESIAN_POINT('Ctrl Pts',(95.290140362784,1.00854760501783,-6.66193841099905));
#22407=CARTESIAN_POINT('Ctrl Pts',(94.9559361902272,0.620746829949751,-6.63556947037964));
#22408=CARTESIAN_POINT('Ctrl Pts',(94.70970373166,-0.507126196349458,-6.58283875118929));
#22409=CARTESIAN_POINT('Ctrl Pts',(95.9314139406376,-1.74640933946404,-6.50374625342801));
#22410=CARTESIAN_POINT('Ctrl Pts',(97.6350683190773,-1.39496882951506,-6.42466091771519));
#22411=CARTESIAN_POINT('Ctrl Pts',(98.2705725016169,0.222956971552548,-6.34557558200236));
#22412=CARTESIAN_POINT('Ctrl Pts',(97.2609102162756,1.63893462213883,-6.26649024628954));
#22413=CARTESIAN_POINT('Ctrl Pts',(95.523548047366,1.56476405676884,-6.18740491057671));
#22414=CARTESIAN_POINT('Ctrl Pts',(94.6379144790523,0.0683724492533236,
-6.10831957486389));
#22415=CARTESIAN_POINT('Ctrl Pts',(95.4089859119762,-1.49024733540083,-6.02923423915106));
#22416=CARTESIAN_POINT('Ctrl Pts',(97.1358852341083,-1.69418316724842,-5.95014890343824));
#22417=CARTESIAN_POINT('Ctrl Pts',(98.2488328103626,-0.358111008410412,
-5.87106356772542));
#22418=CARTESIAN_POINT('Ctrl Pts',(97.7361532112215,1.30349766136748,-5.79197823201259));
#22419=CARTESIAN_POINT('Ctrl Pts',(96.0638825234059,1.78020707787313,-5.71289289629977));
#22420=CARTESIAN_POINT('Ctrl Pts',(94.7521096218384,0.638706772571385,-5.63380756058694));
#22421=CARTESIAN_POINT('Ctrl Pts',(94.993289550825,-1.08340792443364,-5.55472222487413));
#22422=CARTESIAN_POINT('Ctrl Pts',(96.5680961824832,-1.82064515440211,-5.47563688916129));
#22423=CARTESIAN_POINT('Ctrl Pts',(98.0452115487115,-0.903007549691732,
-5.39655155344847));
#22424=CARTESIAN_POINT('Ctrl Pts',(98.0815152372419,0.835696760879677,-5.31746621773565));
#22425=CARTESIAN_POINT('Ctrl Pts',(96.6448751018697,1.81427459898119,-5.23838088202282));
#22426=CARTESIAN_POINT('Ctrl Pts',(95.0393802000608,1.14469652774868,-5.15929554631));
#22427=CARTESIAN_POINT('Ctrl Pts',(94.7283627852766,-0.567354369866243,
-5.08021021059717));
#22428=CARTESIAN_POINT('Ctrl Pts',(95.5670301354957,-1.36034853970369,-5.02748665345529));
#22429=CARTESIAN_POINT('Ctrl Pts',(96.0614639057505,-1.49253166579503,-5.00112487488435));
#22430=CARTESIAN_POINT('',(95.5014043034582,0.825823195401267,-4.99934226694474));
#22431=CARTESIAN_POINT('Ctrl Pts',(96.0619671077198,-1.49064942821852,-4.99999999999999));
#22432=CARTESIAN_POINT('Ctrl Pts',(96.0044903608498,-1.46964766148004,-5.));
#22433=CARTESIAN_POINT('Ctrl Pts',(95.9485815372201,-1.44501993476363,-4.99999999999999));
#22434=CARTESIAN_POINT('Ctrl Pts',(95.8944377879902,-1.41706920437079,-4.99999999999999));
#22435=CARTESIAN_POINT('Ctrl Pts',(95.8402940387602,-1.38911847397796,-4.99999999999999));
#22436=CARTESIAN_POINT('Ctrl Pts',(95.7879146300858,-1.35784372527998,-4.99999999999998));
#22437=CARTESIAN_POINT('Ctrl Pts',(95.7375294374415,-1.32350210039842,-4.99999999999999));
#22438=CARTESIAN_POINT('Ctrl Pts',(95.6994193338114,-1.29752695146327,-4.99999999999999));
#22439=CARTESIAN_POINT('Ctrl Pts',(95.6624507216058,-1.26979620197149,-5.));
#22440=CARTESIAN_POINT('Ctrl Pts',(95.626739354002,-1.2404089680386,-4.99999999999999));
#22441=CARTESIAN_POINT('Ctrl Pts',(95.6076811882898,-1.22472581693859,-4.99999999999998));
#22442=CARTESIAN_POINT('Ctrl Pts',(95.5889813520719,-1.20857073916018,-4.99999999999998));
#22443=CARTESIAN_POINT('Ctrl Pts',(95.5706593721573,-1.19195798019386,-4.99999999999998));
#22444=CARTESIAN_POINT('Ctrl Pts',(95.5629407688328,-1.18495942997258,-4.99999999999998));
#22445=CARTESIAN_POINT('Ctrl Pts',(95.5552893940888,-1.17787965716329,-4.99999999999997));
#22446=CARTESIAN_POINT('Ctrl Pts',(95.5477168724182,-1.17072963197948,-4.99999999999997));
#22447=CARTESIAN_POINT('Ctrl Pts',(95.504650124993,-1.13006572343368,-4.99999999999999));
#22448=CARTESIAN_POINT('Ctrl Pts',(95.4640439159528,-1.0870546361245,-5.));
#22449=CARTESIAN_POINT('Ctrl Pts',(95.4261046731238,-1.0419386282516,-4.99999999999999));
#22450=CARTESIAN_POINT('Ctrl Pts',(95.3889373943342,-0.997740612755019,
-4.99999999999998));
#22451=CARTESIAN_POINT('Ctrl Pts',(95.3543292114615,-0.951521519435711,
-4.99999999999996));
#22452=CARTESIAN_POINT('Ctrl Pts',(95.3225171923515,-0.903486061979851,
-4.99999999999998));
#22453=CARTESIAN_POINT('Ctrl Pts',(95.2912703645555,-0.856304031124319,
-5.));
#22454=CARTESIAN_POINT('Ctrl Pts',(95.2627208389812,-0.807368811665195,
-5.));
#22455=CARTESIAN_POINT('Ctrl Pts',(95.2371412618981,-0.756864590129229,
-4.99999999999998));
#22456=CARTESIAN_POINT('Ctrl Pts',(95.2336088440832,-0.749890197577584,
-4.99999999999998));
#22457=CARTESIAN_POINT('Ctrl Pts',(95.2301331454239,-0.742885878855996,
-4.99999999999998));
#22458=CARTESIAN_POINT('Ctrl Pts',(95.2267149639007,-0.73585211685431,-4.99999999999998));
#22459=CARTESIAN_POINT('Ctrl Pts',(95.2218245699291,-0.725788910129543,
-4.99999999999997));
#22460=CARTESIAN_POINT('Ctrl Pts',(95.2170556886264,-0.715673106931688,
-4.99999999999998));
#22461=CARTESIAN_POINT('Ctrl Pts',(95.2124126352842,-0.705512126926518,
-4.99999999999998));
#22462=CARTESIAN_POINT('Ctrl Pts',(95.1892489299728,-0.654820065223355,
-4.99999999999999));
#22463=CARTESIAN_POINT('Ctrl Pts',(95.1691908098272,-0.602958917485143,
-5.));
#22464=CARTESIAN_POINT('Ctrl Pts',(95.1524510672623,-0.550120264291242,
-4.99999999999999));
#22465=CARTESIAN_POINT('Ctrl Pts',(95.1406599895568,-0.512901969968789,
-4.99999999999997));
#22466=CARTESIAN_POINT('Ctrl Pts',(95.1305162434914,-0.475198299946772,
-4.99999999999999));
#22467=CARTESIAN_POINT('Ctrl Pts',(95.1221096646921,-0.437074027164263,
-4.99999999999999));
#22468=CARTESIAN_POINT('Ctrl Pts',(95.1102087873009,-0.383102928237414,
-5.));
#22469=CARTESIAN_POINT('Ctrl Pts',(95.1017878832149,-0.328287883604904,
-5.00000000000001));
#22470=CARTESIAN_POINT('Ctrl Pts',(95.0967901027504,-0.272945005188943,
-5.));
#22471=CARTESIAN_POINT('Ctrl Pts',(95.0953641741231,-0.257154996962496,
-4.99999999999999));
#22472=CARTESIAN_POINT('Ctrl Pts',(95.0942171752866,-0.241322108062098,
-4.99999999999998));
#22473=CARTESIAN_POINT('Ctrl Pts',(95.0933484296855,-0.225453941639844,
-4.99999999999998));
#22474=CARTESIAN_POINT('Ctrl Pts',(95.0926773352721,-0.213195994293428,
-4.99999999999998));
#22475=CARTESIAN_POINT('Ctrl Pts',(95.0921723561223,-0.200914299570177,
-5.00000000000001));
#22476=CARTESIAN_POINT('Ctrl Pts',(95.0918335220152,-0.188636107436641,
-5.00000000000001));
#22477=CARTESIAN_POINT('Ctrl Pts',(95.0902952695563,-0.132895085968137,
-5.00000000000001));
#22478=CARTESIAN_POINT('Ctrl Pts',(95.0921697597597,-0.0771242598153453,
-4.99999999999998));
#22479=CARTESIAN_POINT('Ctrl Pts',(95.0973480466347,-0.0216419304349217,
-5.));
#22480=CARTESIAN_POINT('Ctrl Pts',(95.1025032536317,0.0335931114889033,
-5.00000000000002));
#22481=CARTESIAN_POINT('Ctrl Pts',(95.1109333654676,0.0885433493664647,
-4.99999999999998));
#22482=CARTESIAN_POINT('Ctrl Pts',(95.1225798921731,0.1428795104336,-4.99999999999999));
#22483=CARTESIAN_POINT('Ctrl Pts',(95.1297471360315,0.176317850167353,-4.99999999999999));
#22484=CARTESIAN_POINT('Ctrl Pts',(95.1381334114814,0.209523261961388,-5.));
#22485=CARTESIAN_POINT('Ctrl Pts',(95.1477331817925,0.242413357936291,-4.99999999999999));
#22486=CARTESIAN_POINT('Ctrl Pts',(95.1527180305541,0.259492115956323,-4.99999999999998));
#22487=CARTESIAN_POINT('Ctrl Pts',(95.1580301804523,0.27648576852378,-5.));
#22488=CARTESIAN_POINT('Ctrl Pts',(95.1636694489763,0.293382161393636,-4.99999999999999));
#22489=CARTESIAN_POINT('Ctrl Pts',(95.1678840387523,0.306009927625527,-4.99999999999999));
#22490=CARTESIAN_POINT('Ctrl Pts',(95.1722821897657,0.318585210618562,-5.));
#22491=CARTESIAN_POINT('Ctrl Pts',(95.1768559904802,0.331082302853865,-5.));
#22492=CARTESIAN_POINT('Ctrl Pts',(95.1953000280353,0.381477335979576,-5.));
#22493=CARTESIAN_POINT('Ctrl Pts',(95.2166211329857,0.430678493749573,-5.00000000000001));
#22494=CARTESIAN_POINT('Ctrl Pts',(95.240774279695,0.478371965785178,-5.00000000000001));
#22495=CARTESIAN_POINT('Ctrl Pts',(95.2570276377204,0.510466296424444,-5.00000000000001));
#22496=CARTESIAN_POINT('Ctrl Pts',(95.2745642988511,0.541877366233536,-5.00000000000001));
#22497=CARTESIAN_POINT('Ctrl Pts',(95.2933797850577,0.572499863819867,-5.));
#22498=CARTESIAN_POINT('Ctrl Pts',(95.3018662740307,0.586311757131528,-5.));
#22499=CARTESIAN_POINT('Ctrl Pts',(95.3106153830304,0.599966301852985,-4.99999999999998));
#22500=CARTESIAN_POINT('Ctrl Pts',(95.3196115901348,0.613430963692222,-4.99999999999998));
#22501=CARTESIAN_POINT('Ctrl Pts',(95.348069797335,0.656024484723174,-4.99999999999998));
#22502=CARTESIAN_POINT('Ctrl Pts',(95.3790237180575,0.696765113806646,-5.00000000000001));
#22503=CARTESIAN_POINT('Ctrl Pts',(95.4124490992335,0.73535259756695,-5.));
#22504=CARTESIAN_POINT('Ctrl Pts',(95.4310001045575,0.756768557280509,-4.99999999999999));
#22505=CARTESIAN_POINT('Ctrl Pts',(95.4503129437851,0.777520633676359,-5.00000000000001));
#22506=CARTESIAN_POINT('Ctrl Pts',(95.4703873188195,0.797551637847658,-5.));
#22507=CARTESIAN_POINT('Ctrl Pts',(95.48024357984,0.80738660432981,-5.));
#22508=CARTESIAN_POINT('Ctrl Pts',(95.49028346793,0.817047668215136,-5.));
#22509=CARTESIAN_POINT('Ctrl Pts',(95.5005012383867,0.826532410909935,-4.99999999999998));
#22510=CARTESIAN_POINT('Ctrl Pts',(95.5023647968546,0.825211298936477,-6.49999999999999));
#22511=CARTESIAN_POINT('Ctrl Pts',(95.465287791204,0.790586303190538,-6.49999999999999));
#22512=CARTESIAN_POINT('Ctrl Pts',(95.4306205888711,0.753694223654168,-6.49999999999999));
#22513=CARTESIAN_POINT('Ctrl Pts',(95.3983634067294,0.714861091992313,-6.49999999999999));
#22514=CARTESIAN_POINT('Ctrl Pts',(95.3648728756,0.674543180804199,-6.49999999999998));
#22515=CARTESIAN_POINT('Ctrl Pts',(95.3339795912397,0.632132434877562,-6.49999999999999));
#22516=CARTESIAN_POINT('Ctrl Pts',(95.3057119559182,0.587944010484693,-6.49999999999999));
#22517=CARTESIAN_POINT('Ctrl Pts',(95.2829274891997,0.552326963870395,-6.5));
#22518=CARTESIAN_POINT('Ctrl Pts',(95.2618492968538,0.515553843547565,-6.5));
#22519=CARTESIAN_POINT('Ctrl Pts',(95.2425087645259,0.477771511851716,-6.49999999999999));
#22520=CARTESIAN_POINT('Ctrl Pts',(95.2337277979766,0.460617620472229,-6.49999999999999));
#22521=CARTESIAN_POINT('Ctrl Pts',(95.2253052381579,0.443255508206861,-6.5));
#22522=CARTESIAN_POINT('Ctrl Pts',(95.2172451705105,0.42569809959244,-6.49999999999999));
#22523=CARTESIAN_POINT('Ctrl Pts',(95.2135756822996,0.417704779096444,-6.49999999999998));
#22524=CARTESIAN_POINT('Ctrl Pts',(95.209982368788,0.409673082119565,-6.49999999999999));
#22525=CARTESIAN_POINT('Ctrl Pts',(95.2064689645341,0.401612534201166,-6.49999999999999));
#22526=CARTESIAN_POINT('Ctrl Pts',(95.184714004968,0.351701712282167,-6.5));
#22527=CARTESIAN_POINT('Ctrl Pts',(95.165979192754,0.300599814091978,-6.49999999999997));
#22528=CARTESIAN_POINT('Ctrl Pts',(95.1502902359844,0.248639171268916,-6.49999999999998));
#22529=CARTESIAN_POINT('Ctrl Pts',(95.1342974905974,0.195672403432671,-6.49999999999999));
#22530=CARTESIAN_POINT('Ctrl Pts',(95.1214690981579,0.141812387425034,-6.50000000000001));
#22531=CARTESIAN_POINT('Ctrl Pts',(95.1118732260187,0.0873765018499251,
-6.5));
#22532=CARTESIAN_POINT('Ctrl Pts',(95.1048940041838,0.0477844652225939,
-6.5));
#22533=CARTESIAN_POINT('Ctrl Pts',(95.0996255705039,0.00788700886965863,
-6.50000000000001));
#22534=CARTESIAN_POINT('Ctrl Pts',(95.0961101241668,-0.0322004775501682,
-6.50000000000001));
#22535=CARTESIAN_POINT('Ctrl Pts',(95.0946964759413,-0.048320650809826,
-6.50000000000001));
#22536=CARTESIAN_POINT('Ctrl Pts',(95.0935664559224,-0.0644715938332609,
-6.5));
#22537=CARTESIAN_POINT('Ctrl Pts',(95.0927234879583,-0.0806459176364314,
-6.5));
#22538=CARTESIAN_POINT('Ctrl Pts',(95.0921920134768,-0.0908435060643399,
-6.5));
#22539=CARTESIAN_POINT('Ctrl Pts',(95.0917751094851,-0.101042304681634,
-6.50000000000001));
#22540=CARTESIAN_POINT('Ctrl Pts',(95.09147320548,-0.111235651179997,-6.50000000000001));
#22541=CARTESIAN_POINT('Ctrl Pts',(95.0897905333277,-0.168048611595366,
-6.49999999999999));
#22542=CARTESIAN_POINT('Ctrl Pts',(95.0916740645112,-0.22473643786415,-6.50000000000001));
#22543=CARTESIAN_POINT('Ctrl Pts',(95.0971821488728,-0.280965948211095,
-6.50000000000001));
#22544=CARTESIAN_POINT('Ctrl Pts',(95.1008218950827,-0.318122450133394,
-6.5));
#22545=CARTESIAN_POINT('Ctrl Pts',(95.1060452317314,-0.355079435484354,
-6.49999999999997));
#22546=CARTESIAN_POINT('Ctrl Pts',(95.1128809155332,-0.391744565936287,
-6.49999999999998));
#22547=CARTESIAN_POINT('Ctrl Pts',(95.1229622858471,-0.445818857318795,
-6.49999999999999));
#22548=CARTESIAN_POINT('Ctrl Pts',(95.1365480764267,-0.499258916074601,
-6.5));
#22549=CARTESIAN_POINT('Ctrl Pts',(95.15341201345,-0.551862544225393,-6.5));
#22550=CARTESIAN_POINT('Ctrl Pts',(95.1580484215608,-0.566324878132217,
-6.49999999999999));
#22551=CARTESIAN_POINT('Ctrl Pts',(95.1629329153471,-0.580723955294647,
-6.49999999999999));
#22552=CARTESIAN_POINT('Ctrl Pts',(95.1680614573946,-0.595055460668329,
-6.49999999999999));
#22553=CARTESIAN_POINT('Ctrl Pts',(95.172427499774,-0.607256191254597,-6.49999999999998));
#22554=CARTESIAN_POINT('Ctrl Pts',(95.1769718397079,-0.619411186056283,
-6.49999999999999));
#22555=CARTESIAN_POINT('Ctrl Pts',(95.1816821868991,-0.63149341392484,-6.49999999999999));
#22556=CARTESIAN_POINT('Ctrl Pts',(95.2025223736644,-0.684949321759963,
-6.5));
#22557=CARTESIAN_POINT('Ctrl Pts',(95.2266387923791,-0.737074044746253,
-6.49999999999999));
#22558=CARTESIAN_POINT('Ctrl Pts',(95.2537356093761,-0.787653241889366,
-6.49999999999999));
#22559=CARTESIAN_POINT('Ctrl Pts',(95.280832426373,-0.838232439032478,-6.49999999999999));
#22560=CARTESIAN_POINT('Ctrl Pts',(95.3109101915958,-0.887266965797818,
-6.49999999999998));
#22561=CARTESIAN_POINT('Ctrl Pts',(95.3437265952813,-0.93453689164767,-6.49999999999999));
#22562=CARTESIAN_POINT('Ctrl Pts',(95.3644390346566,-0.964371832819955,
-6.5));
#22563=CARTESIAN_POINT('Ctrl Pts',(95.3862434920268,-0.993503667320148,
-6.49999999999998));
#22564=CARTESIAN_POINT('Ctrl Pts',(95.4090885081249,-1.02187358457514,-6.49999999999999));
#22565=CARTESIAN_POINT('Ctrl Pts',(95.4201840553492,-1.03565250927805,-6.49999999999999));
#22566=CARTESIAN_POINT('Ctrl Pts',(95.4315251653976,-1.04925165069866,-6.49999999999998));
#22567=CARTESIAN_POINT('Ctrl Pts',(95.4431064930379,-1.0626639234839,-6.49999999999999));
#22568=CARTESIAN_POINT('Ctrl Pts',(95.4503586859564,-1.07106264880577,-6.50000000000001));
#22569=CARTESIAN_POINT('Ctrl Pts',(95.457705080573,-1.07938809381907,-6.49999999999998));
#22570=CARTESIAN_POINT('Ctrl Pts',(95.4651444307094,-1.08763846447625,-6.49999999999998));
#22571=CARTESIAN_POINT('Ctrl Pts',(95.4727475267872,-1.09607043227366,-6.49999999999998));
#22572=CARTESIAN_POINT('Ctrl Pts',(95.4804419218002,-1.10441752546094,-6.5));
#22573=CARTESIAN_POINT('Ctrl Pts',(95.4882237216775,-1.11267593612413,-6.5));
#22574=CARTESIAN_POINT('Ctrl Pts',(95.5296481884137,-1.1566375212592,-6.49999999999998));
#22575=CARTESIAN_POINT('Ctrl Pts',(95.5735639857425,-1.19810830457877,-6.49999999999999));
#22576=CARTESIAN_POINT('Ctrl Pts',(95.6197151559512,-1.23683755194955,-6.49999999999999));
#22577=CARTESIAN_POINT('Ctrl Pts',(95.6520292546319,-1.26395497314833,-6.49999999999999));
#22578=CARTESIAN_POINT('Ctrl Pts',(95.6854403501075,-1.2897280483634,-6.5));
#22579=CARTESIAN_POINT('Ctrl Pts',(95.7198731814153,-1.31406219407389,-6.5));
#22580=CARTESIAN_POINT('Ctrl Pts',(95.7332874249566,-1.32354222068023,-6.5));
#22581=CARTESIAN_POINT('Ctrl Pts',(95.7468588681643,-1.33280488458279,-6.49999999999997));
#22582=CARTESIAN_POINT('Ctrl Pts',(95.7605632855576,-1.34183160585072,-6.49999999999998));
#22583=CARTESIAN_POINT('Ctrl Pts',(95.8113349748999,-1.37527351548072,-6.49999999999998));
#22584=CARTESIAN_POINT('Ctrl Pts',(95.863984835545,-1.40552072986475,-6.5));
#22585=CARTESIAN_POINT('Ctrl Pts',(95.9182746138887,-1.4323100669816,-6.49999999999999));
#22586=CARTESIAN_POINT('Ctrl Pts',(95.9495324392697,-1.44773426739684,-6.49999999999998));
#22587=CARTESIAN_POINT('Ctrl Pts',(95.9813346518669,-1.46201162597775,-6.49999999999999));
#22588=CARTESIAN_POINT('Ctrl Pts',(96.0136410264312,-1.47508602121386,-6.49999999999999));
#22589=CARTESIAN_POINT('Ctrl Pts',(96.0292107636313,-1.48138709648526,-6.49999999999998));
#22590=CARTESIAN_POINT('Ctrl Pts',(96.0448976513391,-1.4874086909893,-6.49999999999999));
#22591=CARTESIAN_POINT('Ctrl Pts',(96.0606948201728,-1.49315277804518,-6.49999999999999));
#22592=CARTESIAN_POINT('Ctrl Pts',(95.5022584080476,0.825087759517108,-4.99934226694474));
#22593=CARTESIAN_POINT('Ctrl Pts',(95.5066224930217,0.830156025949504,-4.99956151129649));
#22594=CARTESIAN_POINT('Ctrl Pts',(95.5110267897309,0.835189667628379,-4.99978075564824));
#22595=CARTESIAN_POINT('Ctrl Pts',(95.5154707437297,0.840188050881734,-4.99999999999999));
#22596=CARTESIAN_POINT('Ctrl Pts',(96.8593706716433,-1.49265850562707,-6.49883138166506));
#22597=CARTESIAN_POINT('Ctrl Pts',(97.3538985322231,-1.36050793369471,-6.47246692892639));
#22598=CARTESIAN_POINT('Ctrl Pts',(98.1927101176,-0.567444892518825,-6.41974069761678));
#22599=CARTESIAN_POINT('Ctrl Pts',(97.8816642045551,1.14476294416278,-6.34065268773623));
#22600=CARTESIAN_POINT('Ctrl Pts',(96.27607609225,1.81437997786543,-6.26156735202342));
#22601=CARTESIAN_POINT('Ctrl Pts',(94.8393525453763,0.835745259019781,-6.18248201631059));
#22602=CARTESIAN_POINT('Ctrl Pts',(94.8756583481607,-0.903059964588701,
-6.10339668059776));
#22603=CARTESIAN_POINT('Ctrl Pts',(96.35285946686,-1.82075086179174,-6.02431134488494));
#22604=CARTESIAN_POINT('Ctrl Pts',(97.9277575306634,-1.08347082117818,-5.94522600917211));
#22605=CARTESIAN_POINT('Ctrl Pts',(98.16895145999,0.638743852593271,-5.86614067345928));
#22606=CARTESIAN_POINT('Ctrl Pts',(96.8571024015692,1.78031043271048,-5.78705533774647));
#22607=CARTESIAN_POINT('Ctrl Pts',(95.1847346256529,1.30357333827821,-5.70797000203363));
#22608=CARTESIAN_POINT('Ctrl Pts',(94.6720252621149,-0.358131798728269,
-5.62888466632083));
#22609=CARTESIAN_POINT('Ctrl Pts',(95.7850374527541,-1.69428152784527,-5.54979933060799));
#22610=CARTESIAN_POINT('Ctrl Pts',(97.5120370344031,-1.49033385341736,-5.47071399489516));
#22611=CARTESIAN_POINT('Ctrl Pts',(98.2831532326639,0.0683764156440079,
-5.39162865918234));
#22612=CARTESIAN_POINT('Ctrl Pts',(97.3974682491448,1.56485490851585,-5.31254332346951));
#22613=CARTESIAN_POINT('Ctrl Pts',(95.6600052081528,1.63902976330342,-5.23345798775669));
#22614=CARTESIAN_POINT('Ctrl Pts',(94.6502843168414,0.222969934548651,-5.15437265204388));
#22615=CARTESIAN_POINT('Ctrl Pts',(95.2858253605478,-1.39504985668874,-5.07528731633104));
#22616=CARTESIAN_POINT('Ctrl Pts',(96.9895786983007,-1.74651069703396,-4.99620198061823));
#22617=CARTESIAN_POINT('Ctrl Pts',(98.2112489397104,-0.507268079750478,
-4.9171166449054));
#22618=CARTESIAN_POINT('Ctrl Pts',(97.965179897774,0.620476460483682,-4.86439308776351));
#22619=CARTESIAN_POINT('Ctrl Pts',(97.6311617451579,1.00829008801941,-4.83803130919258));
#22620=CARTESIAN_POINT('Ctrl Pts',(96.8350765218437,-1.40174899523043,-6.5531598419852));
#22621=CARTESIAN_POINT('Ctrl Pts',(97.2994854466366,-1.27764697810663,-6.52679538924653));
#22622=CARTESIAN_POINT('Ctrl Pts',(98.0872096933796,-0.532884986712179,
-6.47406915793692));
#22623=CARTESIAN_POINT('Ctrl Pts',(97.7951078533155,1.07504181345423,-6.39498114805637));
#22624=CARTESIAN_POINT('Ctrl Pts',(96.2873071643481,1.70387620567681,-6.31589581234354));
#22625=CARTESIAN_POINT('Ctrl Pts',(94.9380864412811,0.7848446732345,-6.23681047663072));
#22626=CARTESIAN_POINT('Ctrl Pts',(94.9721810599645,-0.848059615258915,
-6.1577251409179));
#22627=CARTESIAN_POINT('Ctrl Pts',(96.3594140915549,-1.70985907457065,-6.07863980520507));
#22628=CARTESIAN_POINT('Ctrl Pts',(97.838393891827,-1.01748265207518,-5.99955446949225));
#22629=CARTESIAN_POINT('Ctrl Pts',(98.0648980431881,0.599841524506028,-5.92046913377942));
#22630=CARTESIAN_POINT('Ctrl Pts',(96.8329463994579,1.67188164663409,-5.8413837980666));
#22631=CARTESIAN_POINT('Ctrl Pts',(95.2624332240001,1.22417995157775,-5.76229846235377));
#22632=CARTESIAN_POINT('Ctrl Pts',(94.7809501302615,-0.336319986879062,
-5.68321312664096));
#22633=CARTESIAN_POINT('Ctrl Pts',(95.8261749516296,-1.59109228289083,-5.60412779092812));
#22634=CARTESIAN_POINT('Ctrl Pts',(97.4479926140177,-1.3995659246306,-5.52504245521531));
#22635=CARTESIAN_POINT('Ctrl Pts',(98.1721444223804,0.0642119892561631,
-5.44595711950247));
#22636=CARTESIAN_POINT('Ctrl Pts',(97.3404015749321,1.4695483175986,-5.36687178378965));
#22637=CARTESIAN_POINT('Ctrl Pts',(95.7087577241924,1.53920559538711,-5.28778644807683));
#22638=CARTESIAN_POINT('Ctrl Pts',(94.7605333047936,0.209390078535656,-5.20870111236401));
#22639=CARTESIAN_POINT('Ctrl Pts',(95.3573670856515,-1.31008514508701,-5.12961577665117));
#22640=CARTESIAN_POINT('Ctrl Pts',(96.9573543032989,-1.64014046447823,-5.05053044093836));
#22641=CARTESIAN_POINT('Ctrl Pts',(98.1046194191596,-0.476373208220177,
-4.97144510522553));
#22642=CARTESIAN_POINT('Ctrl Pts',(97.8735370711266,0.582686697438373,-4.91872154808365));
#22643=CARTESIAN_POINT('Ctrl Pts',(97.5598621025699,0.946880758360905,-4.89235976951271));
#22644=CARTESIAN_POINT('Ctrl Pts',(96.8107823720442,-1.31083948483379,-6.60748830230534));
#22645=CARTESIAN_POINT('Ctrl Pts',(97.2450723610501,-1.19478602251856,-6.58112384956667));
#22646=CARTESIAN_POINT('Ctrl Pts',(97.9817092691592,-0.498325080905534,
-6.52839761825706));
#22647=CARTESIAN_POINT('Ctrl Pts',(97.7085515020758,1.00532068274568,-6.44930960837651));
#22648=CARTESIAN_POINT('Ctrl Pts',(96.2985382364459,1.5933724334882,-6.37022427266369));
#22649=CARTESIAN_POINT('Ctrl Pts',(95.0368203371858,0.733944087449216,-6.29113893695086));
#22650=CARTESIAN_POINT('Ctrl Pts',(95.0687037717685,-0.793059265929128,
-6.21205360123804));
#22651=CARTESIAN_POINT('Ctrl Pts',(96.3659687162497,-1.59896728734956,-6.13296826552521));
#22652=CARTESIAN_POINT('Ctrl Pts',(97.7490302529905,-0.951494482972173,
-6.05388292981239));
#22653=CARTESIAN_POINT('Ctrl Pts',(97.9608446263864,0.560939196418784,-5.97479759409956));
#22654=CARTESIAN_POINT('Ctrl Pts',(96.8087903973465,1.56345286055771,-5.89571225838674));
#22655=CARTESIAN_POINT('Ctrl Pts',(95.3401318223472,1.14478656487729,-5.81662692267391));
#22656=CARTESIAN_POINT('Ctrl Pts',(94.8898749984081,-0.314508175029856,
-5.73754158696109));
#22657=CARTESIAN_POINT('Ctrl Pts',(95.8673124505051,-1.48790303793639,-5.65845625124826));
#22658=CARTESIAN_POINT('Ctrl Pts',(97.3839481936324,-1.30879799584384,-5.57937091553545));
#22659=CARTESIAN_POINT('Ctrl Pts',(98.0611356120971,0.0600475628683185,
-5.50028557982261));
#22660=CARTESIAN_POINT('Ctrl Pts',(97.2833349007192,1.37424172668135,-5.4212002441098));
#22661=CARTESIAN_POINT('Ctrl Pts',(95.757510240232,1.43938142747079,-5.34211490839696));
#22662=CARTESIAN_POINT('Ctrl Pts',(94.8707822927458,0.19581022252266,-5.26302957268415));
#22663=CARTESIAN_POINT('Ctrl Pts',(95.4289088107553,-1.22512043348528,-5.18394423697132));
#22664=CARTESIAN_POINT('Ctrl Pts',(96.9251299082968,-1.53377023192249,-5.1048589012585));
#22665=CARTESIAN_POINT('Ctrl Pts',(97.9979898986088,-0.445478336689876,
-5.02577356554567));
#22666=CARTESIAN_POINT('Ctrl Pts',(97.7818942444792,0.544896934393064,-4.97305000840379));
#22667=CARTESIAN_POINT('Ctrl Pts',(97.488562459982,0.885471428702395,-4.94668822983285));
#22668=CARTESIAN_POINT('Ctrl Pts',(96.7864882222446,-1.21992997443715,-6.66181676262547));
#22669=CARTESIAN_POINT('Ctrl Pts',(97.1906592754635,-1.11192506693047,-6.6354523098868));
#22670=CARTESIAN_POINT('Ctrl Pts',(97.8762088449389,-0.463765175098888,
-6.5827260785772));
#22671=CARTESIAN_POINT('Ctrl Pts',(97.621995150836,0.935599552037132,-6.50363806869664));
#22672=CARTESIAN_POINT('Ctrl Pts',(96.3097693085439,1.48286866129958,-6.42455273298382));
#22673=CARTESIAN_POINT('Ctrl Pts',(95.1355542330906,0.683043501663935,-6.34546739727099));
#22674=CARTESIAN_POINT('Ctrl Pts',(95.1652264835723,-0.738058916599343,
-6.26638206155817));
#22675=CARTESIAN_POINT('Ctrl Pts',(96.3725233409445,-1.48807550012847,-6.18729672584535));
#22676=CARTESIAN_POINT('Ctrl Pts',(97.6596666141542,-0.885506313869171,
-6.10821139013252));
#22677=CARTESIAN_POINT('Ctrl Pts',(97.8567912095845,0.522036868331542,-6.02912605441969));
#22678=CARTESIAN_POINT('Ctrl Pts',(96.7846343952353,1.45502407448132,-5.95004071870687));
#22679=CARTESIAN_POINT('Ctrl Pts',(95.4178304206945,1.06539317817682,-5.87095538299404));
#22680=CARTESIAN_POINT('Ctrl Pts',(94.9987998665546,-0.29269636318065,-5.79187004728123));
#22681=CARTESIAN_POINT('Ctrl Pts',(95.9084499493806,-1.38471379298194,-5.71278471156839));
#22682=CARTESIAN_POINT('Ctrl Pts',(97.3199037732469,-1.21803006705708,-5.63369937585557));
#22683=CARTESIAN_POINT('Ctrl Pts',(97.9501268018138,0.0558831364804743,
-5.55461404014274));
#22684=CARTESIAN_POINT('Ctrl Pts',(97.2262682265065,1.2789351357641,-5.47552870442993));
#22685=CARTESIAN_POINT('Ctrl Pts',(95.8062627562716,1.33955725955447,-5.3964433687171));
#22686=CARTESIAN_POINT('Ctrl Pts',(94.9810312806979,0.182230366509664,-5.31735803300428));
#22687=CARTESIAN_POINT('Ctrl Pts',(95.500450535859,-1.14015572188355,-5.23827269729146));
#22688=CARTESIAN_POINT('Ctrl Pts',(96.8929055132947,-1.42739999936675,-5.15918736157863));
#22689=CARTESIAN_POINT('Ctrl Pts',(97.891360378058,-0.414583465159574,-5.0801020258658));
#22690=CARTESIAN_POINT('Ctrl Pts',(97.6902514178318,0.507107171347755,-5.02737846872392));
#22691=CARTESIAN_POINT('Ctrl Pts',(97.4172628173941,0.824062099043887,-5.00101669015298));
#22692=CARTESIAN_POINT('Ctrl Pts',(97.4185971022994,0.825211298936501,-4.99999999999999));
#22693=CARTESIAN_POINT('Ctrl Pts',(97.4554550558806,0.790790868711375,-4.99999999999997));
#22694=CARTESIAN_POINT('Ctrl Pts',(97.4899315734933,0.75413001564445,-4.99999999999998));
#22695=CARTESIAN_POINT('Ctrl Pts',(97.5220265074298,0.71554916654118,-4.99999999999999));
#22696=CARTESIAN_POINT('Ctrl Pts',(97.5555441517723,0.675258098136734,-4.99999999999999));
#22697=CARTESIAN_POINT('Ctrl Pts',(97.5864650020965,0.632872580965763,-4.99999999999998));
#22698=CARTESIAN_POINT('Ctrl Pts',(97.6147608454724,0.588707955597061,-4.99999999999997));
#22699=CARTESIAN_POINT('Ctrl Pts',(97.6377328401419,0.552852882289196,-4.99999999999997));
#22700=CARTESIAN_POINT('Ctrl Pts',(97.6589742582729,0.515824041492352,-4.99999999999997));
#22701=CARTESIAN_POINT('Ctrl Pts',(97.6784530940387,0.477771520420676,-4.99999999999998));
#22702=CARTESIAN_POINT('Ctrl Pts',(97.6872340438242,0.460617657594326,-4.99999999999999));
#22703=CARTESIAN_POINT('Ctrl Pts',(97.6956565880827,0.443255574531325,-5.));
#22704=CARTESIAN_POINT('Ctrl Pts',(97.7037166414093,0.425698195714689,-4.99999999999998));
#22705=CARTESIAN_POINT('Ctrl Pts',(97.7073861170761,0.417704901907484,-4.99999999999997));
#22706=CARTESIAN_POINT('Ctrl Pts',(97.7109794186128,0.409673231731474,-5.));
#22707=CARTESIAN_POINT('Ctrl Pts',(97.7144928114126,0.401612710819986,-5.00000000000001));
#22708=CARTESIAN_POINT('Ctrl Pts',(97.7364622700353,0.351209783867421,-5.00000000000001));
#22709=CARTESIAN_POINT('Ctrl Pts',(97.7553517923287,0.299592241161254,-4.99999999999999));
#22710=CARTESIAN_POINT('Ctrl Pts',(97.7711347217224,0.24710214790481,-4.99999999999999));
#22711=CARTESIAN_POINT('Ctrl Pts',(97.7869025056492,0.194662424700384,-4.99999999999998));
#22712=CARTESIAN_POINT('Ctrl Pts',(97.7995701097015,0.141350806312005,-4.99999999999997));
#22713=CARTESIAN_POINT('Ctrl Pts',(97.8090712523609,0.0874748631209174,
-4.99999999999998));
#22714=CARTESIAN_POINT('Ctrl Pts',(97.8160590828384,0.0478505809339526,
-4.99999999999999));
#22715=CARTESIAN_POINT('Ctrl Pts',(97.8213333251037,0.00792027680426406,
-5.));
#22716=CARTESIAN_POINT('Ctrl Pts',(97.8248516812115,-0.0322003712787191,
-4.99999999999999));
#22717=CARTESIAN_POINT('Ctrl Pts',(97.8262653010745,-0.0483202134177673,
-4.99999999999999));
#22718=CARTESIAN_POINT('Ctrl Pts',(97.82739530449,-0.0644708240410482,-5.));
#22719=CARTESIAN_POINT('Ctrl Pts',(97.8282382678351,-0.0806448146134011,
-4.99999999999999));
#22720=CARTESIAN_POINT('Ctrl Pts',(97.8287697686908,-0.0908427548658557,
-4.99999999999999));
#22721=CARTESIAN_POINT('Ctrl Pts',(97.8291866912673,-0.101041906912261,
-5.00000000000002));
#22722=CARTESIAN_POINT('Ctrl Pts',(97.8294886059173,-0.11123560581186,-5.00000000000002));
#22723=CARTESIAN_POINT('Ctrl Pts',(97.8311712794237,-0.16804857289554,-5.00000000000001));
#22724=CARTESIAN_POINT('Ctrl Pts',(97.8292877502248,-0.224736405431888,
-4.99999999999998));
#22725=CARTESIAN_POINT('Ctrl Pts',(97.823779668819,-0.280965921284123,-4.99999999999997));
#22726=CARTESIAN_POINT('Ctrl Pts',(97.820139920031,-0.318122473102923,-4.99999999999996));
#22727=CARTESIAN_POINT('Ctrl Pts',(97.8149165772873,-0.355079507520968,
-4.99999999999997));
#22728=CARTESIAN_POINT('Ctrl Pts',(97.8080808838596,-0.391744685765442,
-4.99999999999998));
#22729=CARTESIAN_POINT('Ctrl Pts',(97.7979995113489,-0.445818983269784,
-5.));
#22730=CARTESIAN_POINT('Ctrl Pts',(97.7844137192366,-0.499259046888469,
-4.99999999999999));
#22731=CARTESIAN_POINT('Ctrl Pts',(97.7675497811822,-0.551862678807369,
-5.));
#22732=CARTESIAN_POINT('Ctrl Pts',(97.7629133729061,-0.566325013381729,
-5.));
#22733=CARTESIAN_POINT('Ctrl Pts',(97.758028879005,-0.580724091132068,-5.));
#22734=CARTESIAN_POINT('Ctrl Pts',(97.7529003368896,-0.595055597017538,
-5.));
#22735=CARTESIAN_POINT('Ctrl Pts',(97.7485342959591,-0.607256323829169,
-5.00000000000001));
#22736=CARTESIAN_POINT('Ctrl Pts',(97.7439899576327,-0.61941131482884,-4.99999999999998));
#22737=CARTESIAN_POINT('Ctrl Pts',(97.7392796121955,-0.631493538889831,
-4.99999999999998));
#22738=CARTESIAN_POINT('Ctrl Pts',(97.7188419797954,-0.683916881769837,
-5.));
#22739=CARTESIAN_POINT('Ctrl Pts',(97.6952532881221,-0.735059967855329,
-4.99999999999998));
#22740=CARTESIAN_POINT('Ctrl Pts',(97.6687930745268,-0.78472064231593,-4.99999999999999));
#22741=CARTESIAN_POINT('Ctrl Pts',(97.6414632614169,-0.836013385930035,
-5.));
#22742=CARTESIAN_POINT('Ctrl Pts',(97.611069818818,-0.88572557878977,-4.99999999999998));
#22743=CARTESIAN_POINT('Ctrl Pts',(97.5778652315618,-0.933628810807292,
-4.99999999999999));
#22744=CARTESIAN_POINT('Ctrl Pts',(97.55696507361,-0.963780822872587,-5.));
#22745=CARTESIAN_POINT('Ctrl Pts',(97.5349500727209,-0.993215986882425,
-4.99999999999999));
#22746=CARTESIAN_POINT('Ctrl Pts',(97.5118733059413,-1.02187370244541,-4.99999999999999));
#22747=CARTESIAN_POINT('Ctrl Pts',(97.5007777616897,-1.03565262365284,-4.99999999999999));
#22748=CARTESIAN_POINT('Ctrl Pts',(97.4894366547208,-1.04925176160035,-4.99999999999997));
#22749=CARTESIAN_POINT('Ctrl Pts',(97.4778553302579,-1.06266403094416,-4.99999999999998));
#22750=CARTESIAN_POINT('Ctrl Pts',(97.4706031339387,-1.07106276035367,-4.99999999999998));
#22751=CARTESIAN_POINT('Ctrl Pts',(97.4632567358199,-1.07938820935805,-4.99999999999998));
#22752=CARTESIAN_POINT('Ctrl Pts',(97.4558173820803,-1.08763858390813,-4.99999999999999));
#22753=CARTESIAN_POINT('Ctrl Pts',(97.448214291688,-1.09607054529482,-5.));
#22754=CARTESIAN_POINT('Ctrl Pts',(97.4405199025075,-1.10441763214809,-4.99999999999998));
#22755=CARTESIAN_POINT('Ctrl Pts',(97.4327381085711,-1.11267603659566,-4.99999999999998));
#22756=CARTESIAN_POINT('Ctrl Pts',(97.3913123727389,-1.15663896902978,-5.));
#22757=CARTESIAN_POINT('Ctrl Pts',(97.3473951534589,-1.19811094637215,-5.));
#22758=CARTESIAN_POINT('Ctrl Pts',(97.3012424311067,-1.23684121121544,-4.99999999999999));
#22759=CARTESIAN_POINT('Ctrl Pts',(97.268929657142,-1.26395732115855,-4.99999999999999));
#22760=CARTESIAN_POINT('Ctrl Pts',(97.2355199860345,-1.2897291990635,-4.99999999999999));
#22761=CARTESIAN_POINT('Ctrl Pts',(97.2010886685523,-1.31406227375371,-4.99999999999998));
#22762=CARTESIAN_POINT('Ctrl Pts',(97.1876744276178,-1.32354229805831,-4.99999999999997));
#22763=CARTESIAN_POINT('Ctrl Pts',(97.1741029870343,-1.33280495971514,-5.));
#22764=CARTESIAN_POINT('Ctrl Pts',(97.1603985722682,-1.34183167880629,-4.99999999999999));
#22765=CARTESIAN_POINT('Ctrl Pts',(97.109626887535,-1.37527358374674,-4.99999999999998));
#22766=CARTESIAN_POINT('Ctrl Pts',(97.0569770311592,-1.40552079373867,-4.99999999999998));
#22767=CARTESIAN_POINT('Ctrl Pts',(97.0026872565067,-1.43231012699531,-4.99999999999998));
#22768=CARTESIAN_POINT('Ctrl Pts',(96.9714294348054,-1.44773432442092,-4.99999999999998));
#22769=CARTESIAN_POINT('Ctrl Pts',(96.9396272257503,-1.46201168030251,-4.99999999999999));
#22770=CARTESIAN_POINT('Ctrl Pts',(96.9073208545389,-1.47508607318309,-4.99999999999999));
#22771=CARTESIAN_POINT('Ctrl Pts',(96.8916875526902,-1.4814128725953,-4.99999999999999));
#22772=CARTESIAN_POINT('Ctrl Pts',(96.8759361418645,-1.48745790481111,-4.99999999999999));
#22773=CARTESIAN_POINT('Ctrl Pts',(96.8600735756126,-1.49322316678187,-4.99999999999999));
#22774=CARTESIAN_POINT('Ctrl Pts',(96.8589947914343,-1.49064942821851,-6.49999999999999));
#22775=CARTESIAN_POINT('Ctrl Pts',(96.9148518906818,-1.47023947405498,-6.49999999999999));
#22776=CARTESIAN_POINT('Ctrl Pts',(96.969228063587,-1.44640480416822,-6.5));
#22777=CARTESIAN_POINT('Ctrl Pts',(97.021942725396,-1.41942415227612,-6.49999999999999));
#22778=CARTESIAN_POINT('Ctrl Pts',(97.0758376502637,-1.39183941291317,-6.49999999999999));
#22779=CARTESIAN_POINT('Ctrl Pts',(97.1279966319397,-1.36096545034004,-6.49999999999999));
#22780=CARTESIAN_POINT('Ctrl Pts',(97.1781953688626,-1.32705566669257,-6.49999999999998));
#22781=CARTESIAN_POINT('Ctrl Pts',(97.2181578764102,-1.30006056546066,-6.49999999999998));
#22782=CARTESIAN_POINT('Ctrl Pts',(97.2568775916097,-1.27114046090819,-6.49999999999998));
#22783=CARTESIAN_POINT('Ctrl Pts',(97.2942225391991,-1.24040893115648,-6.49999999999999));
#22784=CARTESIAN_POINT('Ctrl Pts',(97.3132807037093,-1.22472577754498,-6.49999999999999));
#22785=CARTESIAN_POINT('Ctrl Pts',(97.3319805387447,-1.20857069716563,-6.5));
#22786=CARTESIAN_POINT('Ctrl Pts',(97.3503025175037,-1.1919579355381,-6.50000000000001));
#22787=CARTESIAN_POINT('Ctrl Pts',(97.3580211211267,-1.18495938348356,-6.50000000000001));
#22788=CARTESIAN_POINT('Ctrl Pts',(97.3656724961627,-1.17787960881166,-6.49999999999999));
#22789=CARTESIAN_POINT('Ctrl Pts',(97.3732450181154,-1.17072958174374,-6.49999999999999));
#22790=CARTESIAN_POINT('Ctrl Pts',(97.4162534779211,-1.13012069956669,-6.49999999999998));
#22791=CARTESIAN_POINT('Ctrl Pts',(97.4568080454813,-1.08717098043465,-6.49999999999999));
#22792=CARTESIAN_POINT('Ctrl Pts',(97.4947031586331,-1.04212172111347,-6.5));
#22793=CARTESIAN_POINT('Ctrl Pts',(97.5319288757374,-0.997868231843363,
-6.50000000000001));
#22794=CARTESIAN_POINT('Ctrl Pts',(97.5665887281823,-0.951587784658056,
-6.5));
#22795=CARTESIAN_POINT('Ctrl Pts',(97.5984446961916,-0.903485955601459,
-6.5));
#22796=CARTESIAN_POINT('Ctrl Pts',(97.6220018485104,-0.867915160403415,
-6.49999999999999));
#22797=CARTESIAN_POINT('Ctrl Pts',(97.6440248688239,-0.831347822374541,
-6.50000000000002));
#22798=CARTESIAN_POINT('Ctrl Pts',(97.6643996535905,-0.793863066977394,
-6.50000000000002));
#22799=CARTESIAN_POINT('Ctrl Pts',(97.6747826326615,-0.774760856317049,
-6.50000000000002));
#22800=CARTESIAN_POINT('Ctrl Pts',(97.684737320669,-0.755420366979109,-6.49999999999998));
#22801=CARTESIAN_POINT('Ctrl Pts',(97.6942469201329,-0.735851988628946,
-6.49999999999999));
#22802=CARTESIAN_POINT('Ctrl Pts',(97.699137314062,-0.725788780493837,-6.5));
#22803=CARTESIAN_POINT('Ctrl Pts',(97.7039061953277,-0.715672975917219,
-6.5));
#22804=CARTESIAN_POINT('Ctrl Pts',(97.708549248637,-0.705511994572704,-6.5));
#22805=CARTESIAN_POINT('Ctrl Pts',(97.7317129543623,-0.654819924922506,
-6.5));
#22806=CARTESIAN_POINT('Ctrl Pts',(97.7517710748817,-0.602958770123721,
-6.49999999999999));
#22807=CARTESIAN_POINT('Ctrl Pts',(97.7685108178151,-0.550120111169122,
-6.5));
#22808=CARTESIAN_POINT('Ctrl Pts',(97.7803018950071,-0.512901815229096,
-6.5));
#22809=CARTESIAN_POINT('Ctrl Pts',(97.790445640772,-0.475198144298214,-6.50000000000002));
#22810=CARTESIAN_POINT('Ctrl Pts',(97.7988522195133,-0.437073871454044,
-6.5));
#22811=CARTESIAN_POINT('Ctrl Pts',(97.8107530971982,-0.383102770735259,
-6.49999999999999));
#22812=CARTESIAN_POINT('Ctrl Pts',(97.8191740018439,-0.32828772595591,-6.50000000000001));
#22813=CARTESIAN_POINT('Ctrl Pts',(97.8241717830776,-0.272944848744542,
-6.50000000000001));
#22814=CARTESIAN_POINT('Ctrl Pts',(97.8255977119158,-0.257154840956551,
-6.50000000000001));
#22815=CARTESIAN_POINT('Ctrl Pts',(97.8267447109837,-0.241321952605189,
-6.49999999999999));
#22816=CARTESIAN_POINT('Ctrl Pts',(97.8276134568352,-0.225453786835658,
-6.49999999999999));
#22817=CARTESIAN_POINT('Ctrl Pts',(97.8282845514555,-0.213195839747077,
-6.49999999999999));
#22818=CARTESIAN_POINT('Ctrl Pts',(97.8287895308168,-0.200914145342743,
-6.50000000000002));
#22819=CARTESIAN_POINT('Ctrl Pts',(97.8291283651393,-0.188635953585735,
-6.50000000000002));
#22820=CARTESIAN_POINT('Ctrl Pts',(97.8306666185408,-0.132894935106274,
-6.50000000000001));
#22821=CARTESIAN_POINT('Ctrl Pts',(97.8287921295153,-0.0771241131303391,
-6.49999999999998));
#22822=CARTESIAN_POINT('Ctrl Pts',(97.8236138439893,-0.0216417887842293,
-6.49999999999998));
#22823=CARTESIAN_POINT('Ctrl Pts',(97.8184586382926,0.0335932485862221,
-6.49999999999998));
#22824=CARTESIAN_POINT('Ctrl Pts',(97.8100285278727,0.0885434810548811,
-6.49999999999998));
#22825=CARTESIAN_POINT('Ctrl Pts',(97.7983820026397,0.142879636166974,-6.49999999999997));
#22826=CARTESIAN_POINT('Ctrl Pts',(97.7912147600914,0.176317970351754,-6.49999999999997));
#22827=CARTESIAN_POINT('Ctrl Pts',(97.7828284861102,0.20952337641607,-6.49999999999998));
#22828=CARTESIAN_POINT('Ctrl Pts',(97.7732287174118,0.242413466567256,-6.49999999999998));
#22829=CARTESIAN_POINT('Ctrl Pts',(97.7682438685886,0.259492224643258,-6.49999999999999));
#22830=CARTESIAN_POINT('Ctrl Pts',(97.7629317185495,0.276485877210698,-6.49999999999999));
#22831=CARTESIAN_POINT('Ctrl Pts',(97.7572924498035,0.29338227003039,-6.49999999999999));
#22832=CARTESIAN_POINT('Ctrl Pts',(97.7530778601672,0.306010035309496,-6.49999999999998));
#22833=CARTESIAN_POINT('Ctrl Pts',(97.7486797092745,0.318585317329429,-6.5));
#22834=CARTESIAN_POINT('Ctrl Pts',(97.7441059086613,0.331082408575578,-6.5));
#22835=CARTESIAN_POINT('Ctrl Pts',(97.7256779487625,0.381433509511468,-6.49999999999998));
#22836=CARTESIAN_POINT('Ctrl Pts',(97.7043779291848,0.430592810395182,-6.49999999999997));
#22837=CARTESIAN_POINT('Ctrl Pts',(97.6802507744572,0.478247335619807,-6.49999999999998));
#22838=CARTESIAN_POINT('Ctrl Pts',(97.6639796936088,0.510385009600785,-6.49999999999999));
#22839=CARTESIAN_POINT('Ctrl Pts',(97.6464219739521,0.541837784449329,-6.5));
#22840=CARTESIAN_POINT('Ctrl Pts',(97.6275821154523,0.57249994485488,-6.49999999999999));
#22841=CARTESIAN_POINT('Ctrl Pts',(97.619095628227,0.586311833759779,-6.49999999999998));
#22842=CARTESIAN_POINT('Ctrl Pts',(97.6103465210592,0.599966374158017,-6.49999999999999));
#22843=CARTESIAN_POINT('Ctrl Pts',(97.6013503158627,0.613431031783383,-6.49999999999999));
#22844=CARTESIAN_POINT('Ctrl Pts',(97.5728921081116,0.656024549342588,-6.49999999999999));
#22845=CARTESIAN_POINT('Ctrl Pts',(97.5419381864423,0.696765175184464,-6.49999999999999));
#22846=CARTESIAN_POINT('Ctrl Pts',(97.508512803874,0.735352656153272,-6.49999999999998));
#22847=CARTESIAN_POINT('Ctrl Pts',(97.4899618010268,0.756768610566281,-6.49999999999998));
#22848=CARTESIAN_POINT('Ctrl Pts',(97.4706489644052,0.777520682032755,-6.5));
#22849=CARTESIAN_POINT('Ctrl Pts',(97.4505745920965,0.797551681714772,-6.49999999999998));
#22850=CARTESIAN_POINT('Ctrl Pts',(97.4407183312139,0.807386647190681,-6.49999999999998));
#22851=CARTESIAN_POINT('Ctrl Pts',(97.4306784432458,0.817047710133597,-6.49999999999998));
#22852=CARTESIAN_POINT('Ctrl Pts',(97.4204606728957,0.82653245194677,-6.49999999999997));
#22853=CARTESIAN_POINT('Origin',(96.460480949577,-1.35113193175836E-15,
-6.49999999999999));
#22854=CARTESIAN_POINT('',(97.6151814879562,-2.,-6.49999999999999));
#22855=CARTESIAN_POINT('',(95.3057804111977,-2.,-6.49999999999999));
#22856=CARTESIAN_POINT('',(97.6151814879562,-2.,-6.49999999999999));
#22857=CARTESIAN_POINT('',(94.1510798728185,-2.7389107125398E-15,-6.49999999999999));
#22858=CARTESIAN_POINT('',(95.3057804111977,-2.,-6.49999999999999));
#22859=CARTESIAN_POINT('',(95.3057804111977,2.,-6.49999999999999));
#22860=CARTESIAN_POINT('',(94.1510798728185,-2.7389107125398E-15,-6.49999999999999));
#22861=CARTESIAN_POINT('',(97.6151814879562,2.,-6.49999999999999));
#22862=CARTESIAN_POINT('',(95.3057804111977,2.,-6.49999999999999));
#22863=CARTESIAN_POINT('',(98.7698820263355,4.52980483257521E-16,-6.49999999999999));
#22864=CARTESIAN_POINT('',(97.6151814879562,2.,-6.49999999999999));
#22865=CARTESIAN_POINT('',(98.7698820263355,4.52980483257521E-16,-6.49999999999999));
#22866=CARTESIAN_POINT('Origin',(94.1510798728185,-2.7389107125398E-15,
-6.49999999999999));
#22867=CARTESIAN_POINT('',(95.3057804111977,-2.,-4.99999999999999));
#22868=CARTESIAN_POINT('',(95.3057804111977,-2.,-6.49999999999999));
#22869=CARTESIAN_POINT('',(94.1510798728185,-2.5552136926677E-15,-4.99999999999999));
#22870=CARTESIAN_POINT('',(95.3057804111977,-2.,-4.99999999999999));
#22871=CARTESIAN_POINT('',(94.1510798728185,-2.7389107125398E-15,-6.49999999999999));
#22872=CARTESIAN_POINT('Origin',(95.3057804111977,2.,-6.49999999999999));
#22873=CARTESIAN_POINT('',(95.3057804111977,2.,-4.99999999999999));
#22874=CARTESIAN_POINT('',(94.1510798728185,-2.5552136926677E-15,-4.99999999999999));
#22875=CARTESIAN_POINT('',(95.3057804111977,2.,-6.49999999999999));
#22876=CARTESIAN_POINT('Origin',(97.6151814879562,2.,-6.49999999999999));
#22877=CARTESIAN_POINT('',(97.6151814879562,2.,-4.99999999999999));
#22878=CARTESIAN_POINT('',(95.3057804111977,2.,-4.99999999999999));
#22879=CARTESIAN_POINT('',(97.6151814879562,2.,-6.49999999999999));
#22880=CARTESIAN_POINT('Origin',(98.7698820263355,5.91758361335666E-16,
-6.49999999999999));
#22881=CARTESIAN_POINT('',(98.7698820263355,6.36677503129625E-16,-4.99999999999999));
#22882=CARTESIAN_POINT('',(97.6151814879562,2.,-4.99999999999999));
#22883=CARTESIAN_POINT('',(98.7698820263355,4.52980483257521E-16,-6.49999999999999));
#22884=CARTESIAN_POINT('Origin',(97.6151814879562,-2.,-6.49999999999999));
#22885=CARTESIAN_POINT('',(97.6151814879562,-2.,-4.99999999999999));
#22886=CARTESIAN_POINT('',(98.7698820263355,6.36677503129624E-16,-4.99999999999999));
#22887=CARTESIAN_POINT('',(97.6151814879562,-2.,-6.49999999999999));
#22888=CARTESIAN_POINT('Origin',(95.3057804111977,-2.,-6.49999999999999));
#22889=CARTESIAN_POINT('',(97.6151814879562,-2.,-4.99999999999999));
#22890=CARTESIAN_POINT('Origin',(96.460480949577,-1.16743491188625E-15,
-4.99999999999999));
#40722=UNCERTAINTY_MEASURE_WITH_UNIT(LENGTH_MEASURE(0.01),#40735,
'DISTANCE_ACCURACY_VALUE',
'Maximum model space distance between geometric entities at asserted c
onnectivities');
#40724=UNCERTAINTY_MEASURE_WITH_UNIT(LENGTH_MEASURE(0.01),#40735,
'DISTANCE_ACCURACY_VALUE',
'Maximum model space distance between geometric entities at asserted c
onnectivities');
#40732=(
GEOMETRIC_REPRESENTATION_CONTEXT(3)
GLOBAL_UNCERTAINTY_ASSIGNED_CONTEXT((#40722))
GLOBAL_UNIT_ASSIGNED_CONTEXT((#40735,#40737,#40738))
REPRESENTATION_CONTEXT('','3D')
);
#40734=(
GEOMETRIC_REPRESENTATION_CONTEXT(3)
GLOBAL_UNCERTAINTY_ASSIGNED_CONTEXT((#40724))
GLOBAL_UNIT_ASSIGNED_CONTEXT((#40735,#40737,#40738))
REPRESENTATION_CONTEXT('','3D')
);
#40735=(
LENGTH_UNIT()
NAMED_UNIT(*)
SI_UNIT(.MILLI.,.METRE.)
);
#40737=(
NAMED_UNIT(*)
PLANE_ANGLE_UNIT()
SI_UNIT($,.RADIAN.)
);
#40738=(
NAMED_UNIT(*)
SI_UNIT($,.STERADIAN.)
SOLID_ANGLE_UNIT()
);
#40746=SHAPE_DEFINITION_REPRESENTATION(#40755,#40772);
#40755=PRODUCT_DEFINITION_SHAPE('',$,#40782);
#40772=SHAPE_REPRESENTATION('',(#3402),#40732);
#40774=PRODUCT_DEFINITION_CONTEXT('part definition',#40803,'design');
#40782=PRODUCT_DEFINITION('Nut (1)','Nut_right',#40791,#40774);
#40791=PRODUCT_DEFINITION_FORMATION('',$,#40812);
#40803=APPLICATION_CONTEXT(
'Core Data for Automotive Mechanical Design Process');
#40804=PRODUCT_CONTEXT('part definition',#40803,'mechanical');
#40812=PRODUCT('Nut (1)','Nut_right',$,(#40804));
#40815=PRESENTATION_STYLE_ASSIGNMENT((#40818));
#40818=SURFACE_STYLE_USAGE(.BOTH.,#40821);
#40821=SURFACE_SIDE_STYLE('',(#40824));
#40824=SURFACE_STYLE_FILL_AREA(#40827);
#40827=FILL_AREA_STYLE('Opaque(203,203,203)',(#40830));
#40830=FILL_AREA_STYLE_COLOUR('Opaque(203,203,203)',#40833);
#40833=COLOUR_RGB('Opaque(203,203,203)', 0.09019608, 0.27058824, 0.51372549);
ENDSEC;
END-ISO-10303-21;
